ISO-10303-21;
HEADER;
/* Generated by software containing ST-Developer
 * from STEP Tools, Inc. (www.steptools.com) 
 */
/* OPTION: using custom renumber hook */

FILE_DESCRIPTION(
/* description */ ('STEP AP242 Edition 2', 'CAx-IF Rec.Pracs.---Representation and Presentation of Product Manufa
cturing Information (PMI)---4.0---2014-10-13', 'CAx-IF Rec.Pracs.---3D Tessellated Geometry---0.4---2014-09-14', '2;1', 'CAx-IF Rec.Pracs.---User Defined Attributes---1.5---2016-08-15'),
/* implementation_level */ '2;1');

FILE_NAME(
/* name */ 'refill_cap.step',
/* time_stamp */ '2026-10-08T12:15:07Z',
/* author */ (''),
/* organization */ (''),
/* preprocessor_version */ 'ST-DEVELOPER v20',
/* originating_system */ 'ONSHAPE BY PTC INC, 1.221',
/* authorisation */ '  ');

FILE_SCHEMA (('AP242_MANAGED_MODEL_BASED_3D_ENGINEERING_MIM_LF { 1 0 10303 442 3 1 4 }'));
ENDSEC;

DATA;
#60=COLOUR_RGB('', 0.66274510, 0.83137255, 0.94901961);
#204=SHAPE_REPRESENTATION_RELATIONSHIP('','',#13778,#231);
#231=ADVANCED_BREP_SHAPE_REPRESENTATION('',(#13722),#45468);
#431=CIRCLE('',#13991,0.000254000000000004);
#432=CIRCLE('',#13992,0.000254000000000037);
#433=CIRCLE('',#13994,0.009236);
#434=CIRCLE('',#13995,0.00076200000000009);
#435=CIRCLE('',#13996,0.0007619999999999);
#436=CIRCLE('',#13999,0.0081692);
#437=CIRCLE('',#14001,0.0081692);
#1092=B_SPLINE_CURVE_WITH_KNOTS('',3,(#27276,#27277,#27278,#27279,#27280,
#27281,#27282,#27283),.UNSPECIFIED.,.F.,.F.,(4,1,1,1,1,4),(0.,0.000509865687280155,
0.00101973137456031,0.00203946274912062,0.00305919412368093,0.00407892549824124),
 .UNSPECIFIED.);
#1093=B_SPLINE_CURVE_WITH_KNOTS('',3,(#27471,#27472,#27473,#27474),
 .UNSPECIFIED.,.F.,.F.,(4,4),(0.,0.00208376980020791),.UNSPECIFIED.);
#1094=B_SPLINE_CURVE_WITH_KNOTS('',3,(#27713,#27714,#27715,#27716,#27717,
#27718,#27719,#27720),.UNSPECIFIED.,.F.,.F.,(4,1,1,1,1,4),(0.,0.00114238418818656,
0.00228476837637312,0.00342715256455968,0.00399834465865296,0.00456953675274624),
 .UNSPECIFIED.);
#1095=B_SPLINE_CURVE_WITH_KNOTS('',3,(#28043,#28044,#28045,#28046,#28047,
#28048),.UNSPECIFIED.,.F.,.F.,(4,1,1,4),(0.,0.00491511497907896,0.00737267246861844,
0.00983022995815793),.UNSPECIFIED.);
#1096=B_SPLINE_CURVE_WITH_KNOTS('',3,(#28227,#28228,#28229,#28230,#28231,
#28232),.UNSPECIFIED.,.F.,.F.,(4,1,1,4),(1.86835436258807E-17,0.00537056638515156,
0.00805584957772733,0.0107411327703031),.UNSPECIFIED.);
#1097=B_SPLINE_CURVE_WITH_KNOTS('',3,(#28493,#28494,#28495,#28496,#28497),
 .UNSPECIFIED.,.F.,.F.,(4,1,4),(0.,0.0044135208761771,0.0088270417523542),
 .UNSPECIFIED.);
#1237=PLANE('',#13997);
#1238=PLANE('',#13998);
#1239=PLANE('',#14000);
#1576=CYLINDRICAL_SURFACE('',#13993,0.009236);
#1577=CYLINDRICAL_SURFACE('',#14002,0.0081692);
#1851=(
BOUNDED_CURVE()
B_SPLINE_CURVE(2,(#27231,#27232,#27233,#27234,#27235,#27236,#27237,#27238,
#27239,#27240,#27241,#27242,#27243,#27244,#27245,#27246,#27247,#27248,#27249,
#27250,#27251,#27252,#27253,#27254,#27255,#27256,#27257,#27258,#27259,#27260,
#27261,#27262,#27263,#27264,#27265,#27266,#27267,#27268,#27269,#27270,#27271,
#27272,#27273),.UNSPECIFIED.,.F.,.F.)
B_SPLINE_CURVE_WITH_KNOTS((3,2,2,2,2,2,2,2,2,2,2,2,2,2,2,2,2,2,2,2,2,3),
(0.253327980224673,0.277777777777778,0.305555555555555,0.333333333333334,
0.361111111111111,0.388888888888889,0.416666666666667,0.444444444444444,
0.472222222222222,0.5,0.527777777777778,0.555555555555556,0.583333333333333,
0.611111111111111,0.638888888888889,0.666666666666667,0.694444444444444,
0.722222222222222,0.75,0.777777777777778,0.805555555555556,0.833333333333333),
 .UNSPECIFIED.)
CURVE()
GEOMETRIC_REPRESENTATION_ITEM()
RATIONAL_B_SPLINE_CURVE((0.992813518121856,0.970008160635222,1.,0.965925826289068,
1.,0.965925826289068,1.,0.965925826289068,1.,0.965925826289068,1.,0.965925826289068,
1.,0.965925826289068,1.,0.965925826289068,1.,0.965925826289068,1.,0.965925826289068,
1.,0.965925826289068,1.,0.965925826289068,1.,0.965925826289068,1.,0.965925826289068,
1.,0.965925826289068,1.,0.965925826289068,1.,0.965925826289068,1.,0.965925826289068,
1.,0.965925826289068,1.,0.965925826289068,1.,0.965925826289068,1.))
REPRESENTATION_ITEM('')
);
#1852=(
BOUNDED_CURVE()
B_SPLINE_CURVE(2,(#27285,#27286,#27287,#27288,#27289),.UNSPECIFIED.,.F.,
 .F.)
B_SPLINE_CURVE_WITH_KNOTS((3,2,3),(0.27956288087666,0.305555555555555,0.333333333333333),
 .UNSPECIFIED.)
CURVE()
GEOMETRIC_REPRESENTATION_ITEM()
RATIONAL_B_SPLINE_CURVE((0.995901974981237,0.968115559160064,1.,0.965925826289069,
1.))
REPRESENTATION_ITEM('')
);
#1853=(
BOUNDED_CURVE()
B_SPLINE_CURVE(2,(#27291,#27292,#27293,#27294,#27295,#27296,#27297,#27298,
#27299,#27300,#27301,#27302,#27303),.UNSPECIFIED.,.F.,.F.)
B_SPLINE_CURVE_WITH_KNOTS((3,2,2,2,2,2,3),(0.333333333333333,0.361111111111111,
0.388888888888889,0.416666666666667,0.444444444444444,0.472222222222222,
0.5),.UNSPECIFIED.)
CURVE()
GEOMETRIC_REPRESENTATION_ITEM()
RATIONAL_B_SPLINE_CURVE((1.,0.965925826289068,1.,0.965925826289068,1.,0.965925826289068,
1.,0.965925826289068,1.,0.965925826289068,1.,0.965925826289068,1.))
REPRESENTATION_ITEM('')
);
#1854=(
BOUNDED_CURVE()
B_SPLINE_CURVE(2,(#27305,#27306,#27307,#27308,#27309,#27310,#27311,#27312,
#27313,#27314,#27315,#27316,#27317),.UNSPECIFIED.,.F.,.F.)
B_SPLINE_CURVE_WITH_KNOTS((3,2,2,2,2,2,3),(0.5,0.527777777777778,0.555555555555556,
0.583333333333333,0.611111111111111,0.638888888888889,0.666666666666666),
 .UNSPECIFIED.)
CURVE()
GEOMETRIC_REPRESENTATION_ITEM()
RATIONAL_B_SPLINE_CURVE((1.,0.965925826289069,1.,0.965925826289068,1.,0.965925826289068,
1.,0.965925826289068,1.,0.965925826289068,1.,0.965925826289069,1.))
REPRESENTATION_ITEM('')
);
#1855=(
BOUNDED_CURVE()
B_SPLINE_CURVE(2,(#27319,#27320,#27321,#27322,#27323,#27324,#27325,#27326,
#27327,#27328,#27329,#27330,#27331),.UNSPECIFIED.,.F.,.F.)
B_SPLINE_CURVE_WITH_KNOTS((3,2,2,2,2,2,3),(0.666666666666666,0.694444444444444,
0.722222222222222,0.75,0.777777777777778,0.805555555555556,0.833333333333333),
 .UNSPECIFIED.)
CURVE()
GEOMETRIC_REPRESENTATION_ITEM()
RATIONAL_B_SPLINE_CURVE((1.,0.965925826289068,1.,0.965925826289068,1.,0.965925826289068,
1.,0.965925826289068,1.,0.965925826289068,1.,0.965925826289068,1.))
REPRESENTATION_ITEM('')
);
#1856=(
BOUNDED_CURVE()
B_SPLINE_CURVE(2,(#27424,#27425,#27426,#27427,#27428,#27429,#27430,#27431,
#27432,#27433,#27434,#27435,#27436,#27437,#27438,#27439,#27440,#27441,#27442,
#27443,#27444,#27445,#27446,#27447,#27448,#27449,#27450,#27451,#27452,#27453,
#27454,#27455,#27456,#27457,#27458,#27459,#27460,#27461,#27462,#27463,#27464,
#27465,#27466,#27467,#27468),.UNSPECIFIED.,.F.,.F.)
B_SPLINE_CURVE_WITH_KNOTS((3,2,2,2,2,2,2,2,2,2,2,2,2,2,2,2,2,2,2,2,2,2,
3),(0.241197850932585,0.25,0.277777777777778,0.305555555555555,0.333333333333334,
0.361111111111111,0.388888888888889,0.416666666666667,0.444444444444444,
0.472222222222222,0.5,0.527777777777778,0.555555555555556,0.583333333333333,
0.611111111111111,0.638888888888889,0.666666666666667,0.694444444444444,
0.722222222222222,0.75,0.777777777777778,0.805555555555556,0.833333333333333),
 .UNSPECIFIED.)
CURVE()
GEOMETRIC_REPRESENTATION_ITEM()
RATIONAL_B_SPLINE_CURVE((0.985248192939002,0.989202665571305,1.,0.965925826289068,
1.,0.965925826289068,1.,0.965925826289068,1.,0.965925826289068,1.,0.965925826289068,
1.,0.965925826289068,1.,0.965925826289068,1.,0.965925826289068,1.,0.965925826289068,
1.,0.965925826289068,1.,0.965925826289068,1.,0.965925826289068,1.,0.965925826289068,
1.,0.965925826289068,1.,0.965925826289068,1.,0.965925826289068,1.,0.965925826289068,
1.,0.965925826289068,1.,0.965925826289068,1.,0.965925826289068,1.,0.965925826289068,
1.))
REPRESENTATION_ITEM('')
);
#1857=(
BOUNDED_CURVE()
B_SPLINE_CURVE(2,(#27664,#27665,#27666,#27667,#27668,#27669,#27670,#27671,
#27672,#27673,#27674,#27675,#27676,#27677,#27678,#27679,#27680,#27681,#27682,
#27683,#27684,#27685,#27686,#27687,#27688,#27689,#27690,#27691,#27692,#27693,
#27694,#27695,#27696,#27697,#27698,#27699,#27700,#27701,#27702,#27703,#27704,
#27705,#27706,#27707,#27708,#27709,#27710),.UNSPECIFIED.,.F.,.F.)
B_SPLINE_CURVE_WITH_KNOTS((3,2,2,2,2,2,2,2,2,2,2,2,2,2,2,2,2,2,2,2,2,2,
2,3),(0.214924305846367,0.222222222222222,0.25,0.277777777777778,0.305555555555555,
0.333333333333334,0.361111111111111,0.388888888888889,0.416666666666667,
0.444444444444444,0.472222222222222,0.5,0.527777777777778,0.555555555555556,
0.583333333333333,0.611111111111111,0.638888888888889,0.666666666666667,
0.694444444444444,0.722222222222222,0.75,0.777777777777778,0.805555555555556,
0.833333333333333),.UNSPECIFIED.)
CURVE()
GEOMETRIC_REPRESENTATION_ITEM()
RATIONAL_B_SPLINE_CURVE((0.98679962630025,0.991047863068525,1.,0.965925826289068,
1.,0.965925826289068,1.,0.965925826289068,1.,0.965925826289068,1.,0.965925826289068,
1.,0.965925826289068,1.,0.965925826289068,1.,0.965925826289068,1.,0.965925826289068,
1.,0.965925826289068,1.,0.965925826289068,1.,0.965925826289068,1.,0.965925826289068,
1.,0.965925826289068,1.,0.965925826289068,1.,0.965925826289068,1.,0.965925826289068,
1.,0.965925826289068,1.,0.965925826289068,1.,0.965925826289068,1.,0.965925826289068,
1.,0.965925826289068,1.))
REPRESENTATION_ITEM('')
);
#1858=(
BOUNDED_CURVE()
B_SPLINE_CURVE(2,(#27723,#27724,#27725,#27726,#27727,#27728,#27729,#27730,
#27731,#27732,#27733,#27734,#27735,#27736,#27737,#27738,#27739,#27740,#27741,
#27742,#27743,#27744,#27745,#27746,#27747,#27748,#27749,#27750,#27751,#27752,
#27753,#27754,#27755,#27756,#27757,#27758,#27759,#27760,#27761,#27762,#27763,
#27764,#27765,#27766,#27767,#27768,#27769,#27770,#27771),.UNSPECIFIED.,
 .F.,.F.)
B_SPLINE_CURVE_WITH_KNOTS((3,2,2,2,2,2,2,2,2,2,2,2,2,2,2,2,2,2,2,2,2,2,
2,2,3),(0.178312023944365,0.194444444444445,0.222222222222222,0.25,0.277777777777778,
0.305555555555555,0.333333333333334,0.361111111111111,0.388888888888889,
0.416666666666667,0.444444444444444,0.472222222222222,0.5,0.527777777777778,
0.555555555555556,0.583333333333334,0.611111111111111,0.638888888888889,
0.666666666666667,0.694444444444444,0.722222222222222,0.75,0.777777777777778,
0.805555555555556,0.833333333333333),.UNSPECIFIED.)
CURVE()
GEOMETRIC_REPRESENTATION_ITEM()
RATIONAL_B_SPLINE_CURVE((0.983407467343328,0.980210839654089,1.,0.965925826289068,
1.,0.965925826289068,1.,0.965925826289068,1.,0.965925826289068,1.,0.965925826289068,
1.,0.965925826289068,1.,0.965925826289068,1.,0.965925826289068,1.,0.965925826289068,
1.,0.965925826289068,1.,0.965925826289068,1.,0.965925826289068,1.,0.965925826289068,
1.,0.965925826289068,1.,0.965925826289068,1.,0.965925826289068,1.,0.965925826289068,
1.,0.965925826289068,1.,0.965925826289068,1.,0.965925826289068,1.,0.965925826289068,
1.,0.965925826289068,1.,0.965925826289068,1.))
REPRESENTATION_ITEM('')
);
#1859=(
BOUNDED_CURVE()
B_SPLINE_CURVE(2,(#27988,#27989,#27990,#27991,#27992,#27993,#27994,#27995,
#27996,#27997,#27998,#27999,#28000,#28001,#28002,#28003,#28004,#28005,#28006,
#28007,#28008,#28009,#28010,#28011,#28012,#28013,#28014,#28015,#28016,#28017,
#28018,#28019,#28020,#28021,#28022,#28023,#28024,#28025,#28026,#28027,#28028,
#28029,#28030,#28031,#28032,#28033,#28034,#28035,#28036,#28037,#28038,#28039,
#28040),.UNSPECIFIED.,.F.,.F.)
B_SPLINE_CURVE_WITH_KNOTS((3,2,2,2,2,2,2,2,2,2,2,2,2,2,2,2,2,2,2,2,2,2,
2,2,2,2,3),(0.121758697158625,0.138888888888889,0.166666666666667,0.194444444444445,
0.222222222222222,0.25,0.277777777777778,0.305555555555555,0.333333333333334,
0.361111111111111,0.388888888888889,0.416666666666667,0.444444444444444,
0.472222222222222,0.5,0.527777777777778,0.555555555555556,0.583333333333333,
0.611111111111111,0.638888888888889,0.666666666666667,0.694444444444444,
0.722222222222222,0.75,0.777777777777778,0.805555555555556,0.833333333333334),
 .UNSPECIFIED.)
CURVE()
GEOMETRIC_REPRESENTATION_ITEM()
RATIONAL_B_SPLINE_CURVE((0.983890809673563,0.978986903366131,1.,0.965925826289068,
1.,0.965925826289068,1.,0.965925826289068,1.,0.965925826289068,1.,0.965925826289068,
1.,0.965925826289068,1.,0.965925826289068,1.,0.965925826289068,1.,0.965925826289068,
1.,0.965925826289068,1.,0.965925826289068,1.,0.965925826289068,1.,0.965925826289068,
1.,0.965925826289068,1.,0.965925826289068,1.,0.965925826289068,1.,0.965925826289068,
1.,0.965925826289068,1.,0.965925826289068,1.,0.965925826289068,1.,0.965925826289068,
1.,0.965925826289068,1.,0.965925826289068,1.,0.965925826289068,1.,0.965925826289068,
1.))
REPRESENTATION_ITEM('')
);
#1860=(
BOUNDED_CURVE()
B_SPLINE_CURVE(2,(#28168,#28169,#28170,#28171,#28172,#28173,#28174,#28175,
#28176,#28177,#28178,#28179,#28180,#28181,#28182,#28183,#28184,#28185,#28186,
#28187,#28188,#28189,#28190,#28191,#28192,#28193,#28194,#28195,#28196,#28197,
#28198,#28199,#28200,#28201,#28202,#28203,#28204,#28205,#28206,#28207,#28208,
#28209,#28210,#28211,#28212,#28213,#28214,#28215,#28216,#28217,#28218,#28219,
#28220,#28221,#28222,#28223,#28224),.UNSPECIFIED.,.F.,.F.)
B_SPLINE_CURVE_WITH_KNOTS((3,2,2,2,2,2,2,2,2,2,2,2,2,2,2,2,2,2,2,2,2,2,
2,2,2,2,2,2,3),(0.0566003037608321,0.0833333333333333,0.111111111111111,
0.138888888888889,0.166666666666667,0.194444444444445,0.222222222222222,
0.25,0.277777777777778,0.305555555555555,0.333333333333334,0.361111111111111,
0.388888888888889,0.416666666666667,0.444444444444444,0.472222222222222,
0.5,0.527777777777778,0.555555555555556,0.583333333333333,0.611111111111111,
0.638888888888889,0.666666666666667,0.694444444444444,0.722222222222222,
0.75,0.777777777777778,0.805555555555556,0.833333333333333),
 .UNSPECIFIED.)
CURVE()
GEOMETRIC_REPRESENTATION_ITEM()
RATIONAL_B_SPLINE_CURVE((0.997533278365187,0.967207387834976,1.,0.965925826289068,
1.,0.965925826289068,1.,0.965925826289068,1.,0.965925826289068,1.,0.965925826289068,
1.,0.965925826289068,1.,0.965925826289068,1.,0.965925826289068,1.,0.965925826289068,
1.,0.965925826289068,1.,0.965925826289068,1.,0.965925826289068,1.,0.965925826289068,
1.,0.965925826289068,1.,0.965925826289068,1.,0.965925826289068,1.,0.965925826289068,
1.,0.965925826289068,1.,0.965925826289068,1.,0.965925826289068,1.,0.965925826289068,
1.,0.965925826289068,1.,0.965925826289068,1.,0.965925826289068,1.,0.965925826289068,
1.,0.965925826289068,1.,0.965925826289068,1.))
REPRESENTATION_ITEM('')
);
#1861=(
BOUNDED_CURVE()
B_SPLINE_CURVE(2,(#28478,#28479,#28480,#28481,#28482,#28483,#28484,#28485,
#28486,#28487,#28488,#28489,#28490),.UNSPECIFIED.,.F.,.F.)
B_SPLINE_CURVE_WITH_KNOTS((3,2,2,2,2,2,3),(0.,0.0277777777777779,0.0555555555555558,
0.0833333333333336,0.111111111111111,0.138888888888889,0.166666666666668),
 .UNSPECIFIED.)
CURVE()
GEOMETRIC_REPRESENTATION_ITEM()
RATIONAL_B_SPLINE_CURVE((1.,0.965925826289068,1.,0.965925826289068,1.,0.965925826289068,
1.,0.965925826289068,1.,0.965925826289068,1.,0.965925826289068,1.))
REPRESENTATION_ITEM('')
);
#1862=(
BOUNDED_CURVE()
B_SPLINE_CURVE(2,(#28500,#28501,#28502,#28503,#28504,#28505,#28506,#28507,
#28508,#28509,#28510,#28511,#28512),.UNSPECIFIED.,.F.,.F.)
B_SPLINE_CURVE_WITH_KNOTS((3,2,2,2,2,2,3),(0.666666666666666,0.694444444444444,
0.722222222222222,0.75,0.777777777777778,0.805555555555556,0.833333333333333),
 .UNSPECIFIED.)
CURVE()
GEOMETRIC_REPRESENTATION_ITEM()
RATIONAL_B_SPLINE_CURVE((1.,0.965925826289068,1.,0.965925826289068,1.,0.965925826289068,
1.,0.965925826289068,1.,0.965925826289068,1.,0.965925826289068,1.))
REPRESENTATION_ITEM('')
);
#1863=(
BOUNDED_CURVE()
B_SPLINE_CURVE(2,(#28514,#28515,#28516,#28517,#28518,#28519,#28520,#28521,
#28522,#28523,#28524,#28525,#28526),.UNSPECIFIED.,.F.,.F.)
B_SPLINE_CURVE_WITH_KNOTS((3,2,2,2,2,2,3),(0.5,0.527777777777778,0.555555555555556,
0.583333333333333,0.611111111111111,0.638888888888889,0.666666666666666),
 .UNSPECIFIED.)
CURVE()
GEOMETRIC_REPRESENTATION_ITEM()
RATIONAL_B_SPLINE_CURVE((1.,0.965925826289069,1.,0.965925826289068,1.,0.965925826289068,
1.,0.965925826289068,1.,0.965925826289068,1.,0.965925826289069,1.))
REPRESENTATION_ITEM('')
);
#1864=(
BOUNDED_CURVE()
B_SPLINE_CURVE(2,(#28528,#28529,#28530,#28531,#28532,#28533,#28534,#28535,
#28536,#28537,#28538,#28539,#28540),.UNSPECIFIED.,.F.,.F.)
B_SPLINE_CURVE_WITH_KNOTS((3,2,2,2,2,2,3),(0.333333333333333,0.361111111111111,
0.388888888888889,0.416666666666667,0.444444444444444,0.472222222222222,
0.5),.UNSPECIFIED.)
CURVE()
GEOMETRIC_REPRESENTATION_ITEM()
RATIONAL_B_SPLINE_CURVE((1.,0.965925826289068,1.,0.965925826289068,1.,0.965925826289068,
1.,0.965925826289068,1.,0.965925826289068,1.,0.965925826289068,1.))
REPRESENTATION_ITEM('')
);
#1865=(
BOUNDED_CURVE()
B_SPLINE_CURVE(2,(#28542,#28543,#28544,#28545,#28546,#28547,#28548,#28549,
#28550,#28551,#28552,#28553,#28554),.UNSPECIFIED.,.F.,.F.)
B_SPLINE_CURVE_WITH_KNOTS((3,2,2,2,2,2,3),(0.166666666666668,0.194444444444445,
0.222222222222222,0.25,0.277777777777778,0.305555555555555,0.333333333333333),
 .UNSPECIFIED.)
CURVE()
GEOMETRIC_REPRESENTATION_ITEM()
RATIONAL_B_SPLINE_CURVE((1.,0.965925826289069,1.,0.965925826289068,1.,0.965925826289068,
1.,0.965925826289068,1.,0.965925826289068,1.,0.965925826289069,1.))
REPRESENTATION_ITEM('')
);
#2352=ORIENTED_EDGE('',*,*,#5823,.F.);
#2353=ORIENTED_EDGE('',*,*,#5824,.T.);
#2354=ORIENTED_EDGE('',*,*,#5825,.T.);
#2355=ORIENTED_EDGE('',*,*,#5826,.T.);
#2356=ORIENTED_EDGE('',*,*,#5827,.T.);
#2357=ORIENTED_EDGE('',*,*,#5828,.T.);
#2358=ORIENTED_EDGE('',*,*,#5829,.T.);
#2359=ORIENTED_EDGE('',*,*,#5830,.F.);
#2360=ORIENTED_EDGE('',*,*,#5831,.T.);
#2361=ORIENTED_EDGE('',*,*,#5823,.T.);
#2362=ORIENTED_EDGE('',*,*,#5832,.T.);
#2363=ORIENTED_EDGE('',*,*,#5833,.F.);
#2364=ORIENTED_EDGE('',*,*,#5834,.T.);
#2365=ORIENTED_EDGE('',*,*,#5830,.T.);
#2366=ORIENTED_EDGE('',*,*,#5835,.T.);
#2367=ORIENTED_EDGE('',*,*,#5836,.F.);
#2368=ORIENTED_EDGE('',*,*,#5837,.T.);
#2369=ORIENTED_EDGE('',*,*,#5833,.T.);
#2370=ORIENTED_EDGE('',*,*,#5838,.T.);
#2371=ORIENTED_EDGE('',*,*,#5839,.F.);
#2372=ORIENTED_EDGE('',*,*,#5840,.T.);
#2373=ORIENTED_EDGE('',*,*,#5836,.T.);
#2374=ORIENTED_EDGE('',*,*,#5841,.T.);
#2375=ORIENTED_EDGE('',*,*,#5842,.F.);
#2376=ORIENTED_EDGE('',*,*,#5843,.T.);
#2377=ORIENTED_EDGE('',*,*,#5839,.T.);
#2378=ORIENTED_EDGE('',*,*,#5844,.T.);
#2379=ORIENTED_EDGE('',*,*,#5845,.F.);
#2380=ORIENTED_EDGE('',*,*,#5846,.T.);
#2381=ORIENTED_EDGE('',*,*,#5842,.T.);
#2382=ORIENTED_EDGE('',*,*,#5847,.T.);
#2383=ORIENTED_EDGE('',*,*,#5848,.F.);
#2384=ORIENTED_EDGE('',*,*,#5849,.F.);
#2385=ORIENTED_EDGE('',*,*,#5850,.F.);
#2386=ORIENTED_EDGE('',*,*,#5851,.F.);
#2387=ORIENTED_EDGE('',*,*,#5829,.F.);
#2388=ORIENTED_EDGE('',*,*,#5852,.F.);
#2389=ORIENTED_EDGE('',*,*,#5847,.F.);
#2390=ORIENTED_EDGE('',*,*,#5844,.F.);
#2391=ORIENTED_EDGE('',*,*,#5841,.F.);
#2392=ORIENTED_EDGE('',*,*,#5838,.F.);
#2393=ORIENTED_EDGE('',*,*,#5835,.F.);
#2394=ORIENTED_EDGE('',*,*,#5832,.F.);
#2395=ORIENTED_EDGE('',*,*,#5853,.T.);
#2396=ORIENTED_EDGE('',*,*,#5824,.F.);
#2397=ORIENTED_EDGE('',*,*,#5831,.F.);
#2398=ORIENTED_EDGE('',*,*,#5834,.F.);
#2399=ORIENTED_EDGE('',*,*,#5837,.F.);
#2400=ORIENTED_EDGE('',*,*,#5840,.F.);
#2401=ORIENTED_EDGE('',*,*,#5843,.F.);
#2402=ORIENTED_EDGE('',*,*,#5846,.F.);
#2403=ORIENTED_EDGE('',*,*,#5854,.F.);
#2404=ORIENTED_EDGE('',*,*,#5826,.F.);
#2405=ORIENTED_EDGE('',*,*,#5825,.F.);
#2406=ORIENTED_EDGE('',*,*,#5853,.F.);
#2407=ORIENTED_EDGE('',*,*,#5845,.T.);
#2408=ORIENTED_EDGE('',*,*,#5851,.T.);
#2409=ORIENTED_EDGE('',*,*,#5850,.T.);
#2410=ORIENTED_EDGE('',*,*,#5849,.T.);
#2411=ORIENTED_EDGE('',*,*,#5848,.T.);
#2412=ORIENTED_EDGE('',*,*,#5852,.T.);
#2413=ORIENTED_EDGE('',*,*,#5828,.F.);
#2414=ORIENTED_EDGE('',*,*,#5827,.F.);
#2415=ORIENTED_EDGE('',*,*,#5854,.T.);
#5823=EDGE_CURVE('',#7617,#7618,#1851,.T.);
#5824=EDGE_CURVE('',#7617,#7619,#1092,.T.);
#5825=EDGE_CURVE('',#7619,#7620,#1852,.T.);
#5826=EDGE_CURVE('',#7620,#7621,#1853,.T.);
#5827=EDGE_CURVE('',#7621,#7622,#1854,.T.);
#5828=EDGE_CURVE('',#7622,#7623,#1855,.T.);
#5829=EDGE_CURVE('',#7623,#7618,#431,.T.);
#5830=EDGE_CURVE('',#7624,#7625,#1856,.T.);
#5831=EDGE_CURVE('',#7624,#7617,#1093,.T.);
#5832=EDGE_CURVE('',#7618,#7625,#8817,.T.);
#5833=EDGE_CURVE('',#7626,#7627,#1857,.T.);
#5834=EDGE_CURVE('',#7626,#7624,#1094,.T.);
#5835=EDGE_CURVE('',#7625,#7627,#432,.T.);
#5836=EDGE_CURVE('',#7628,#7629,#1858,.T.);
#5837=EDGE_CURVE('',#7628,#7626,#433,.F.);
#5838=EDGE_CURVE('',#7627,#7629,#8818,.T.);
#5839=EDGE_CURVE('',#7630,#7631,#1859,.T.);
#5840=EDGE_CURVE('',#7630,#7628,#1095,.T.);
#5841=EDGE_CURVE('',#7629,#7631,#434,.T.);
#5842=EDGE_CURVE('',#7632,#7633,#1860,.T.);
#5843=EDGE_CURVE('',#7632,#7630,#1096,.T.);
#5844=EDGE_CURVE('',#7631,#7633,#8819,.T.);
#5845=EDGE_CURVE('',#7634,#7635,#1861,.T.);
#5846=EDGE_CURVE('',#7634,#7632,#1097,.T.);
#5847=EDGE_CURVE('',#7633,#7636,#435,.T.);
#5848=EDGE_CURVE('',#7637,#7636,#1862,.T.);
#5849=EDGE_CURVE('',#7638,#7637,#1863,.T.);
#5850=EDGE_CURVE('',#7639,#7638,#1864,.T.);
#5851=EDGE_CURVE('',#7635,#7639,#1865,.T.);
#5852=EDGE_CURVE('',#7636,#7623,#8820,.T.);
#5853=EDGE_CURVE('',#7634,#7619,#436,.T.);
#5854=EDGE_CURVE('',#7640,#7640,#437,.T.);
#7617=VERTEX_POINT('',#27274);
#7618=VERTEX_POINT('',#27275);
#7619=VERTEX_POINT('',#27284);
#7620=VERTEX_POINT('',#27290);
#7621=VERTEX_POINT('',#27304);
#7622=VERTEX_POINT('',#27318);
#7623=VERTEX_POINT('',#27332);
#7624=VERTEX_POINT('',#27469);
#7625=VERTEX_POINT('',#27470);
#7626=VERTEX_POINT('',#27711);
#7627=VERTEX_POINT('',#27712);
#7628=VERTEX_POINT('',#27772);
#7629=VERTEX_POINT('',#27773);
#7630=VERTEX_POINT('',#28041);
#7631=VERTEX_POINT('',#28042);
#7632=VERTEX_POINT('',#28225);
#7633=VERTEX_POINT('',#28226);
#7634=VERTEX_POINT('',#28491);
#7635=VERTEX_POINT('',#28492);
#7636=VERTEX_POINT('',#28499);
#7637=VERTEX_POINT('',#28513);
#7638=VERTEX_POINT('',#28527);
#7639=VERTEX_POINT('',#28541);
#7640=VERTEX_POINT('',#28561);
#8817=LINE('',#27475,#9645);
#8818=LINE('',#27775,#9646);
#8819=LINE('',#28233,#9647);
#8820=LINE('',#28556,#9648);
#9645=VECTOR('',#15719,1.);
#9646=VECTOR('',#15726,1.);
#9647=VECTOR('',#15729,1.);
#9648=VECTOR('',#15734,1.);
#10629=EDGE_LOOP('',(#2352,#2353,#2354,#2355,#2356,#2357,#2358));
#10630=EDGE_LOOP('',(#2359,#2360,#2361,#2362));
#10631=EDGE_LOOP('',(#2363,#2364,#2365,#2366));
#10632=EDGE_LOOP('',(#2367,#2368,#2369,#2370));
#10633=EDGE_LOOP('',(#2371,#2372,#2373,#2374));
#10634=EDGE_LOOP('',(#2375,#2376,#2377,#2378));
#10635=EDGE_LOOP('',(#2379,#2380,#2381,#2382,#2383,#2384,#2385,#2386));
#10636=EDGE_LOOP('',(#2387,#2388,#2389,#2390,#2391,#2392,#2393,#2394));
#10637=EDGE_LOOP('',(#2395,#2396,#2397,#2398,#2399,#2400,#2401,#2402));
#10638=EDGE_LOOP('',(#2403));
#10639=EDGE_LOOP('',(#2404,#2405,#2406,#2407,#2408,#2409,#2410,#2411,#2412,
#2413,#2414));
#10640=EDGE_LOOP('',(#2415));
#11744=FACE_BOUND('',#10629,.T.);
#11745=FACE_BOUND('',#10630,.T.);
#11746=FACE_BOUND('',#10631,.T.);
#11747=FACE_BOUND('',#10632,.T.);
#11748=FACE_BOUND('',#10633,.T.);
#11749=FACE_BOUND('',#10634,.T.);
#11750=FACE_BOUND('',#10635,.T.);
#11751=FACE_BOUND('',#10636,.T.);
#11752=FACE_BOUND('',#10637,.T.);
#11753=FACE_BOUND('',#10638,.T.);
#11754=FACE_BOUND('',#10639,.T.);
#11755=FACE_BOUND('',#10640,.T.);
#12668=(
BOUNDED_SURFACE()
B_SPLINE_SURFACE(3,2,((#27051,#27052,#27053,#27054,#27055,#27056,#27057,
#27058,#27059,#27060,#27061,#27062,#27063,#27064,#27065,#27066,#27067,#27068,
#27069,#27070,#27071,#27072,#27073,#27074,#27075,#27076,#27077,#27078,#27079,
#27080,#27081,#27082,#27083,#27084,#27085,#27086,#27087,#27088,#27089,#27090,
#27091,#27092,#27093,#27094,#27095),(#27096,#27097,#27098,#27099,#27100,
#27101,#27102,#27103,#27104,#27105,#27106,#27107,#27108,#27109,#27110,#27111,
#27112,#27113,#27114,#27115,#27116,#27117,#27118,#27119,#27120,#27121,#27122,
#27123,#27124,#27125,#27126,#27127,#27128,#27129,#27130,#27131,#27132,#27133,
#27134,#27135,#27136,#27137,#27138,#27139,#27140),(#27141,#27142,#27143,
#27144,#27145,#27146,#27147,#27148,#27149,#27150,#27151,#27152,#27153,#27154,
#27155,#27156,#27157,#27158,#27159,#27160,#27161,#27162,#27163,#27164,#27165,
#27166,#27167,#27168,#27169,#27170,#27171,#27172,#27173,#27174,#27175,#27176,
#27177,#27178,#27179,#27180,#27181,#27182,#27183,#27184,#27185),(#27186,
#27187,#27188,#27189,#27190,#27191,#27192,#27193,#27194,#27195,#27196,#27197,
#27198,#27199,#27200,#27201,#27202,#27203,#27204,#27205,#27206,#27207,#27208,
#27209,#27210,#27211,#27212,#27213,#27214,#27215,#27216,#27217,#27218,#27219,
#27220,#27221,#27222,#27223,#27224,#27225,#27226,#27227,#27228,#27229,#27230)),
 .UNSPECIFIED.,.F.,.F.,.F.)
B_SPLINE_SURFACE_WITH_KNOTS((4,4),(3,2,2,2,2,2,2,2,2,2,2,2,2,2,2,2,2,2,
2,2,2,2,3),(0.,1.),(0.249847948106021,0.25,0.277777777777778,0.305555555555555,
0.333333333333334,0.361111111111111,0.388888888888889,0.416666666666667,
0.444444444444444,0.472222222222222,0.5,0.527777777777778,0.555555555555556,
0.583333333333333,0.611111111111111,0.638888888888889,0.666666666666667,
0.694444444444444,0.722222222222222,0.75,0.777777777777778,0.805555555555556,
0.833333333333333),.PIECEWISE_BEZIER_KNOTS.)
GEOMETRIC_REPRESENTATION_ITEM()
RATIONAL_B_SPLINE_SURFACE(((0.99962900687411,0.999813482464653,1.,0.965925826289068,
1.,0.965925826289068,1.,0.965925826289068,1.,0.965925826289068,1.,0.965925826289068,
1.,0.965925826289068,1.,0.965925826289068,1.,0.965925826289068,1.,0.965925826289068,
1.,0.965925826289068,1.,0.965925826289068,1.,0.965925826289068,1.,0.965925826289068,
1.,0.965925826289068,1.,0.965925826289068,1.,0.965925826289068,1.,0.965925826289068,
1.,0.965925826289068,1.,0.965925826289068,1.,0.965925826289068,1.,0.965925826289068,
1.),(0.843716499555672,0.84387220241987,0.844029628745984,0.81527001655892,
0.844029628745984,0.81527001655892,0.844029628745984,0.81527001655892,0.844029628745984,
0.81527001655892,0.844029628745984,0.81527001655892,0.844029628745984,0.81527001655892,
0.844029628745984,0.81527001655892,0.844029628745984,0.81527001655892,0.844029628745984,
0.81527001655892,0.844029628745984,0.81527001655892,0.844029628745984,0.81527001655892,
0.844029628745984,0.81527001655892,0.844029628745984,0.81527001655892,0.844029628745984,
0.81527001655892,0.844029628745984,0.81527001655892,0.844029628745984,0.81527001655892,
0.844029628745984,0.81527001655892,0.844029628745984,0.81527001655892,0.844029628745984,
0.81527001655892,0.844029628745984,0.81527001655892,0.844029628745984,0.81527001655892,
0.844029628745984),(0.843716499555672,0.84387220241987,0.844029628745984,
0.81527001655892,0.844029628745984,0.81527001655892,0.844029628745984,0.81527001655892,
0.844029628745984,0.81527001655892,0.844029628745984,0.81527001655892,0.844029628745984,
0.81527001655892,0.844029628745984,0.81527001655892,0.844029628745984,0.81527001655892,
0.844029628745984,0.81527001655892,0.844029628745984,0.81527001655892,0.844029628745984,
0.81527001655892,0.844029628745984,0.81527001655892,0.844029628745984,0.81527001655892,
0.844029628745984,0.81527001655892,0.844029628745984,0.81527001655892,0.844029628745984,
0.81527001655892,0.844029628745984,0.81527001655892,0.844029628745984,0.81527001655892,
0.844029628745984,0.81527001655892,0.844029628745984,0.81527001655892,0.844029628745984,
0.81527001655892,0.844029628745984),(0.99962900687411,0.999813482464653,
1.,0.965925826289068,1.,0.965925826289068,1.,0.965925826289068,1.,0.965925826289068,
1.,0.965925826289068,1.,0.965925826289068,1.,0.965925826289068,1.,0.965925826289068,
1.,0.965925826289068,1.,0.965925826289068,1.,0.965925826289068,1.,0.965925826289068,
1.,0.965925826289068,1.,0.965925826289068,1.,0.965925826289068,1.,0.965925826289068,
1.,0.965925826289068,1.,0.965925826289068,1.,0.965925826289068,1.,0.965925826289068,
1.,0.965925826289068,1.)))
REPRESENTATION_ITEM('')
SURFACE()
);
#12669=(
BOUNDED_SURFACE()
B_SPLINE_SURFACE(1,2,((#27334,#27335,#27336,#27337,#27338,#27339,#27340,
#27341,#27342,#27343,#27344,#27345,#27346,#27347,#27348,#27349,#27350,#27351,
#27352,#27353,#27354,#27355,#27356,#27357,#27358,#27359,#27360,#27361,#27362,
#27363,#27364,#27365,#27366,#27367,#27368,#27369,#27370,#27371,#27372,#27373,
#27374,#27375,#27376,#27377,#27378),(#27379,#27380,#27381,#27382,#27383,
#27384,#27385,#27386,#27387,#27388,#27389,#27390,#27391,#27392,#27393,#27394,
#27395,#27396,#27397,#27398,#27399,#27400,#27401,#27402,#27403,#27404,#27405,
#27406,#27407,#27408,#27409,#27410,#27411,#27412,#27413,#27414,#27415,#27416,
#27417,#27418,#27419,#27420,#27421,#27422,#27423)),.RULED_SURF.,.F.,.F.,
 .F.)
B_SPLINE_SURFACE_WITH_KNOTS((2,2),(3,2,2,2,2,2,2,2,2,2,2,2,2,2,2,2,2,2,
2,2,2,2,3),(0.,1.),(0.23764503803818,0.25,0.277777777777778,0.305555555555555,
0.333333333333334,0.361111111111111,0.388888888888889,0.416666666666667,
0.444444444444444,0.472222222222222,0.5,0.527777777777778,0.555555555555556,
0.583333333333333,0.611111111111111,0.638888888888889,0.666666666666667,
0.694444444444444,0.722222222222222,0.75,0.777777777777778,0.805555555555556,
0.833333333333333),.PIECEWISE_BEZIER_KNOTS.)
GEOMETRIC_REPRESENTATION_ITEM()
RATIONAL_B_SPLINE_SURFACE(((0.983170724690329,0.984844535677156,1.,0.965925826289068,
1.,0.965925826289068,1.,0.965925826289068,1.,0.965925826289068,1.,0.965925826289068,
1.,0.965925826289068,1.,0.965925826289068,1.,0.965925826289068,1.,0.965925826289068,
1.,0.965925826289068,1.,0.965925826289068,1.,0.965925826289068,1.,0.965925826289068,
1.,0.965925826289068,1.,0.965925826289068,1.,0.965925826289068,1.,0.965925826289068,
1.,0.965925826289068,1.,0.965925826289068,1.,0.965925826289068,1.,0.965925826289068,
1.),(0.983170724690329,0.984844535677156,1.,0.965925826289068,1.,0.965925826289068,
1.,0.965925826289068,1.,0.965925826289068,1.,0.965925826289068,1.,0.965925826289068,
1.,0.965925826289068,1.,0.965925826289068,1.,0.965925826289068,1.,0.965925826289068,
1.,0.965925826289068,1.,0.965925826289068,1.,0.965925826289068,1.,0.965925826289068,
1.,0.965925826289068,1.,0.965925826289068,1.,0.965925826289068,1.,0.965925826289068,
1.,0.965925826289068,1.,0.965925826289068,1.,0.965925826289068,1.)))
REPRESENTATION_ITEM('')
SURFACE()
);
#12670=(
BOUNDED_SURFACE()
B_SPLINE_SURFACE(3,2,((#27476,#27477,#27478,#27479,#27480,#27481,#27482,
#27483,#27484,#27485,#27486,#27487,#27488,#27489,#27490,#27491,#27492,#27493,
#27494,#27495,#27496,#27497,#27498,#27499,#27500,#27501,#27502,#27503,#27504,
#27505,#27506,#27507,#27508,#27509,#27510,#27511,#27512,#27513,#27514,#27515,
#27516,#27517,#27518,#27519,#27520,#27521,#27522),(#27523,#27524,#27525,
#27526,#27527,#27528,#27529,#27530,#27531,#27532,#27533,#27534,#27535,#27536,
#27537,#27538,#27539,#27540,#27541,#27542,#27543,#27544,#27545,#27546,#27547,
#27548,#27549,#27550,#27551,#27552,#27553,#27554,#27555,#27556,#27557,#27558,
#27559,#27560,#27561,#27562,#27563,#27564,#27565,#27566,#27567,#27568,#27569),
(#27570,#27571,#27572,#27573,#27574,#27575,#27576,#27577,#27578,#27579,
#27580,#27581,#27582,#27583,#27584,#27585,#27586,#27587,#27588,#27589,#27590,
#27591,#27592,#27593,#27594,#27595,#27596,#27597,#27598,#27599,#27600,#27601,
#27602,#27603,#27604,#27605,#27606,#27607,#27608,#27609,#27610,#27611,#27612,
#27613,#27614,#27615,#27616),(#27617,#27618,#27619,#27620,#27621,#27622,
#27623,#27624,#27625,#27626,#27627,#27628,#27629,#27630,#27631,#27632,#27633,
#27634,#27635,#27636,#27637,#27638,#27639,#27640,#27641,#27642,#27643,#27644,
#27645,#27646,#27647,#27648,#27649,#27650,#27651,#27652,#27653,#27654,#27655,
#27656,#27657,#27658,#27659,#27660,#27661,#27662,#27663)),.UNSPECIFIED.,
 .F.,.F.,.F.)
B_SPLINE_SURFACE_WITH_KNOTS((4,4),(3,2,2,2,2,2,2,2,2,2,2,2,2,2,2,2,2,2,
2,2,2,2,2,3),(0.,1.),(0.211213851681445,0.222222222222222,0.25,0.277777777777778,
0.305555555555555,0.333333333333334,0.361111111111111,0.388888888888889,
0.416666666666667,0.444444444444444,0.472222222222222,0.5,0.527777777777778,
0.555555555555556,0.583333333333333,0.611111111111111,0.638888888888889,
0.666666666666667,0.694444444444444,0.722222222222222,0.75,0.777777777777778,
0.805555555555556,0.833333333333333),.PIECEWISE_BEZIER_KNOTS.)
GEOMETRIC_REPRESENTATION_ITEM()
RATIONAL_B_SPLINE_SURFACE(((0.983695740414847,0.986496359317093,1.,0.965925826289068,
1.,0.965925826289068,1.,0.965925826289068,1.,0.965925826289068,1.,0.965925826289068,
1.,0.965925826289068,1.,0.965925826289068,1.,0.965925826289068,1.,0.965925826289068,
1.,0.965925826289068,1.,0.965925826289068,1.,0.965925826289068,1.,0.965925826289068,
1.,0.965925826289068,1.,0.965925826289068,1.,0.965925826289068,1.,0.965925826289068,
1.,0.965925826289068,1.,0.965925826289068,1.,0.965925826289068,1.,0.965925826289068,
1.,0.965925826289068,1.),(0.830268350581347,0.832632155913669,0.844029628745982,
0.815270016558918,0.844029628745982,0.815270016558918,0.844029628745982,
0.815270016558918,0.844029628745982,0.815270016558918,0.844029628745982,
0.815270016558918,0.844029628745982,0.815270016558918,0.844029628745982,
0.815270016558918,0.844029628745982,0.815270016558918,0.844029628745982,
0.815270016558918,0.844029628745982,0.815270016558918,0.844029628745982,
0.815270016558918,0.844029628745982,0.815270016558918,0.844029628745982,
0.815270016558918,0.844029628745982,0.815270016558918,0.844029628745982,
0.815270016558918,0.844029628745982,0.815270016558918,0.844029628745982,
0.815270016558918,0.844029628745982,0.815270016558918,0.844029628745982,
0.815270016558918,0.844029628745982,0.815270016558918,0.844029628745982,
0.815270016558918,0.844029628745982,0.815270016558918,0.844029628745982),
(0.830268350581347,0.832632155913669,0.844029628745982,0.815270016558918,
0.844029628745982,0.815270016558918,0.844029628745982,0.815270016558918,
0.844029628745982,0.815270016558918,0.844029628745982,0.815270016558918,
0.844029628745982,0.815270016558918,0.844029628745982,0.815270016558918,
0.844029628745982,0.815270016558918,0.844029628745982,0.815270016558918,
0.844029628745982,0.815270016558918,0.844029628745982,0.815270016558918,
0.844029628745982,0.815270016558918,0.844029628745982,0.815270016558918,
0.844029628745982,0.815270016558918,0.844029628745982,0.815270016558918,
0.844029628745982,0.815270016558918,0.844029628745982,0.815270016558918,
0.844029628745982,0.815270016558918,0.844029628745982,0.815270016558918,
0.844029628745982,0.815270016558918,0.844029628745982,0.815270016558918,
0.844029628745982,0.815270016558918,0.844029628745982),(0.983695740414847,
0.986496359317093,1.,0.965925826289068,1.,0.965925826289068,1.,0.965925826289068,
1.,0.965925826289068,1.,0.965925826289068,1.,0.965925826289068,1.,0.965925826289068,
1.,0.965925826289068,1.,0.965925826289068,1.,0.965925826289068,1.,0.965925826289068,
1.,0.965925826289068,1.,0.965925826289068,1.,0.965925826289068,1.,0.965925826289068,
1.,0.965925826289068,1.,0.965925826289068,1.,0.965925826289068,1.,0.965925826289068,
1.,0.965925826289068,1.,0.965925826289068,1.,0.965925826289068,1.)))
REPRESENTATION_ITEM('')
SURFACE()
);
#12671=(
BOUNDED_SURFACE()
B_SPLINE_SURFACE(3,2,((#27776,#27777,#27778,#27779,#27780,#27781,#27782,
#27783,#27784,#27785,#27786,#27787,#27788,#27789,#27790,#27791,#27792,#27793,
#27794,#27795,#27796,#27797,#27798,#27799,#27800,#27801,#27802,#27803,#27804,
#27805,#27806,#27807,#27808,#27809,#27810,#27811,#27812,#27813,#27814,#27815,
#27816,#27817,#27818,#27819,#27820,#27821,#27822,#27823,#27824,#27825,#27826,
#27827,#27828),(#27829,#27830,#27831,#27832,#27833,#27834,#27835,#27836,
#27837,#27838,#27839,#27840,#27841,#27842,#27843,#27844,#27845,#27846,#27847,
#27848,#27849,#27850,#27851,#27852,#27853,#27854,#27855,#27856,#27857,#27858,
#27859,#27860,#27861,#27862,#27863,#27864,#27865,#27866,#27867,#27868,#27869,
#27870,#27871,#27872,#27873,#27874,#27875,#27876,#27877,#27878,#27879,#27880,
#27881),(#27882,#27883,#27884,#27885,#27886,#27887,#27888,#27889,#27890,
#27891,#27892,#27893,#27894,#27895,#27896,#27897,#27898,#27899,#27900,#27901,
#27902,#27903,#27904,#27905,#27906,#27907,#27908,#27909,#27910,#27911,#27912,
#27913,#27914,#27915,#27916,#27917,#27918,#27919,#27920,#27921,#27922,#27923,
#27924,#27925,#27926,#27927,#27928,#27929,#27930,#27931,#27932,#27933,#27934),
(#27935,#27936,#27937,#27938,#27939,#27940,#27941,#27942,#27943,#27944,
#27945,#27946,#27947,#27948,#27949,#27950,#27951,#27952,#27953,#27954,#27955,
#27956,#27957,#27958,#27959,#27960,#27961,#27962,#27963,#27964,#27965,#27966,
#27967,#27968,#27969,#27970,#27971,#27972,#27973,#27974,#27975,#27976,#27977,
#27978,#27979,#27980,#27981,#27982,#27983,#27984,#27985,#27986,#27987)),
 .UNSPECIFIED.,.F.,.F.,.F.)
B_SPLINE_SURFACE_WITH_KNOTS((4,4),(3,2,2,2,2,2,2,2,2,2,2,2,2,2,2,2,2,2,
2,2,2,2,2,2,2,2,3),(0.,1.),(0.117489249341577,0.138888888888889,0.166666666666667,
0.194444444444445,0.222222222222222,0.25,0.277777777777778,0.305555555555555,
0.333333333333334,0.361111111111111,0.388888888888889,0.416666666666667,
0.444444444444444,0.472222222222222,0.5,0.527777777777778,0.555555555555556,
0.583333333333333,0.611111111111111,0.638888888888889,0.666666666666667,
0.694444444444444,0.722222222222222,0.75,0.777777777777778,0.805555555555556,
0.833333333333333),.PIECEWISE_BEZIER_KNOTS.)
GEOMETRIC_REPRESENTATION_ITEM()
RATIONAL_B_SPLINE_SURFACE(((0.987945180393274,0.973749698729688,1.,0.965925826289068,
1.,0.965925826289068,1.,0.965925826289068,1.,0.965925826289068,1.,0.965925826289068,
1.,0.965925826289068,1.,0.965925826289068,1.,0.965925826289068,1.,0.965925826289068,
1.,0.965925826289068,1.,0.965925826289068,1.,0.965925826289068,1.,0.965925826289068,
1.,0.965925826289068,1.,0.965925826289068,1.,0.965925826289068,1.,0.965925826289068,
1.,0.965925826289068,1.,0.965925826289068,1.,0.965925826289068,1.,0.965925826289068,
1.,0.965925826289068,1.,0.965925826289068,1.,0.965925826289068,1.,0.965925826289068,
1.),(0.937809947736769,0.92433484387349,0.949253021674191,0.916908009318038,
0.949253021674191,0.916908009318038,0.949253021674191,0.916908009318038,
0.949253021674191,0.916908009318038,0.949253021674191,0.916908009318038,
0.949253021674191,0.916908009318038,0.949253021674191,0.916908009318038,
0.949253021674191,0.916908009318038,0.949253021674191,0.916908009318038,
0.949253021674191,0.916908009318038,0.949253021674191,0.916908009318038,
0.949253021674191,0.916908009318038,0.949253021674191,0.916908009318038,
0.949253021674191,0.916908009318038,0.949253021674191,0.916908009318038,
0.949253021674191,0.916908009318038,0.949253021674191,0.916908009318038,
0.949253021674191,0.916908009318038,0.949253021674191,0.916908009318038,
0.949253021674191,0.916908009318038,0.949253021674191,0.916908009318038,
0.949253021674191,0.916908009318038,0.949253021674191,0.916908009318038,
0.949253021674191,0.916908009318038,0.949253021674191,0.916908009318038,
0.949253021674191),(0.937809947736769,0.92433484387349,0.949253021674191,
0.916908009318038,0.949253021674191,0.916908009318038,0.949253021674191,
0.916908009318038,0.949253021674191,0.916908009318038,0.949253021674191,
0.916908009318038,0.949253021674191,0.916908009318038,0.949253021674191,
0.916908009318038,0.949253021674191,0.916908009318038,0.949253021674191,
0.916908009318038,0.949253021674191,0.916908009318038,0.949253021674191,
0.916908009318038,0.949253021674191,0.916908009318038,0.949253021674191,
0.916908009318038,0.949253021674191,0.916908009318038,0.949253021674191,
0.916908009318038,0.949253021674191,0.916908009318038,0.949253021674191,
0.916908009318038,0.949253021674191,0.916908009318038,0.949253021674191,
0.916908009318038,0.949253021674191,0.916908009318038,0.949253021674191,
0.916908009318038,0.949253021674191,0.916908009318038,0.949253021674191,
0.916908009318038,0.949253021674191,0.916908009318038,0.949253021674191,
0.916908009318038,0.949253021674191),(0.987945180393274,0.973749698729688,
1.,0.965925826289068,1.,0.965925826289068,1.,0.965925826289068,1.,0.965925826289068,
1.,0.965925826289068,1.,0.965925826289068,1.,0.965925826289068,1.,0.965925826289068,
1.,0.965925826289068,1.,0.965925826289068,1.,0.965925826289068,1.,0.965925826289068,
1.,0.965925826289068,1.,0.965925826289068,1.,0.965925826289068,1.,0.965925826289068,
1.,0.965925826289068,1.,0.965925826289068,1.,0.965925826289068,1.,0.965925826289068,
1.,0.965925826289068,1.,0.965925826289068,1.,0.965925826289068,1.,0.965925826289068,
1.,0.965925826289068,1.)))
REPRESENTATION_ITEM('')
SURFACE()
);
#12672=(
BOUNDED_SURFACE()
B_SPLINE_SURFACE(1,2,((#28050,#28051,#28052,#28053,#28054,#28055,#28056,
#28057,#28058,#28059,#28060,#28061,#28062,#28063,#28064,#28065,#28066,#28067,
#28068,#28069,#28070,#28071,#28072,#28073,#28074,#28075,#28076,#28077,#28078,
#28079,#28080,#28081,#28082,#28083,#28084,#28085,#28086,#28087,#28088,#28089,
#28090,#28091,#28092,#28093,#28094,#28095,#28096,#28097,#28098,#28099,#28100,
#28101,#28102,#28103,#28104,#28105,#28106,#28107,#28108),(#28109,#28110,
#28111,#28112,#28113,#28114,#28115,#28116,#28117,#28118,#28119,#28120,#28121,
#28122,#28123,#28124,#28125,#28126,#28127,#28128,#28129,#28130,#28131,#28132,
#28133,#28134,#28135,#28136,#28137,#28138,#28139,#28140,#28141,#28142,#28143,
#28144,#28145,#28146,#28147,#28148,#28149,#28150,#28151,#28152,#28153,#28154,
#28155,#28156,#28157,#28158,#28159,#28160,#28161,#28162,#28163,#28164,#28165,
#28166,#28167)),.RULED_SURF.,.F.,.F.,.F.)
B_SPLINE_SURFACE_WITH_KNOTS((2,2),(3,2,2,2,2,2,2,2,2,2,2,2,2,2,2,2,2,2,
2,2,2,2,2,2,2,2,2,2,2,3),(0.,1.),(0.051939905583397,0.0555555555555556,
0.0833333333333333,0.111111111111111,0.138888888888889,0.166666666666667,
0.194444444444445,0.222222222222222,0.25,0.277777777777778,0.305555555555555,
0.333333333333334,0.361111111111111,0.388888888888889,0.416666666666667,
0.444444444444444,0.472222222222222,0.5,0.527777777777778,0.555555555555556,
0.583333333333333,0.611111111111111,0.638888888888889,0.666666666666667,
0.694444444444444,0.722222222222222,0.75,0.777777777777778,0.805555555555556,
0.833333333333333),.PIECEWISE_BEZIER_KNOTS.)
GEOMETRIC_REPRESENTATION_ITEM()
RATIONAL_B_SPLINE_SURFACE(((0.992284183551064,0.995564789731747,1.,0.965925826289068,
1.,0.965925826289068,1.,0.965925826289068,1.,0.965925826289068,1.,0.965925826289068,
1.,0.965925826289068,1.,0.965925826289068,1.,0.965925826289068,1.,0.965925826289068,
1.,0.965925826289068,1.,0.965925826289068,1.,0.965925826289068,1.,0.965925826289068,
1.,0.965925826289068,1.,0.965925826289068,1.,0.965925826289068,1.,0.965925826289068,
1.,0.965925826289068,1.,0.965925826289068,1.,0.965925826289068,1.,0.965925826289068,
1.,0.965925826289068,1.,0.965925826289068,1.,0.965925826289068,1.,0.965925826289068,
1.,0.965925826289068,1.,0.965925826289068,1.,0.965925826289068,1.),(0.992284183551064,
0.995564789731747,1.,0.965925826289068,1.,0.965925826289068,1.,0.965925826289068,
1.,0.965925826289068,1.,0.965925826289068,1.,0.965925826289068,1.,0.965925826289068,
1.,0.965925826289068,1.,0.965925826289068,1.,0.965925826289068,1.,0.965925826289068,
1.,0.965925826289068,1.,0.965925826289068,1.,0.965925826289068,1.,0.965925826289068,
1.,0.965925826289068,1.,0.965925826289068,1.,0.965925826289068,1.,0.965925826289068,
1.,0.965925826289068,1.,0.965925826289068,1.,0.965925826289068,1.,0.965925826289068,
1.,0.965925826289068,1.,0.965925826289068,1.,0.965925826289068,1.,0.965925826289068,
1.,0.965925826289068,1.)))
REPRESENTATION_ITEM('')
SURFACE()
);
#12673=(
BOUNDED_SURFACE()
B_SPLINE_SURFACE(3,2,((#28234,#28235,#28236,#28237,#28238,#28239,#28240,
#28241,#28242,#28243,#28244,#28245,#28246,#28247,#28248,#28249,#28250,#28251,
#28252,#28253,#28254,#28255,#28256,#28257,#28258,#28259,#28260,#28261,#28262,
#28263,#28264,#28265,#28266,#28267,#28268,#28269,#28270,#28271,#28272,#28273,
#28274,#28275,#28276,#28277,#28278,#28279,#28280,#28281,#28282,#28283,#28284,
#28285,#28286,#28287,#28288,#28289,#28290,#28291,#28292,#28293,#28294),
(#28295,#28296,#28297,#28298,#28299,#28300,#28301,#28302,#28303,#28304,
#28305,#28306,#28307,#28308,#28309,#28310,#28311,#28312,#28313,#28314,#28315,
#28316,#28317,#28318,#28319,#28320,#28321,#28322,#28323,#28324,#28325,#28326,
#28327,#28328,#28329,#28330,#28331,#28332,#28333,#28334,#28335,#28336,#28337,
#28338,#28339,#28340,#28341,#28342,#28343,#28344,#28345,#28346,#28347,#28348,
#28349,#28350,#28351,#28352,#28353,#28354,#28355),(#28356,#28357,#28358,
#28359,#28360,#28361,#28362,#28363,#28364,#28365,#28366,#28367,#28368,#28369,
#28370,#28371,#28372,#28373,#28374,#28375,#28376,#28377,#28378,#28379,#28380,
#28381,#28382,#28383,#28384,#28385,#28386,#28387,#28388,#28389,#28390,#28391,
#28392,#28393,#28394,#28395,#28396,#28397,#28398,#28399,#28400,#28401,#28402,
#28403,#28404,#28405,#28406,#28407,#28408,#28409,#28410,#28411,#28412,#28413,
#28414,#28415,#28416),(#28417,#28418,#28419,#28420,#28421,#28422,#28423,
#28424,#28425,#28426,#28427,#28428,#28429,#28430,#28431,#28432,#28433,#28434,
#28435,#28436,#28437,#28438,#28439,#28440,#28441,#28442,#28443,#28444,#28445,
#28446,#28447,#28448,#28449,#28450,#28451,#28452,#28453,#28454,#28455,#28456,
#28457,#28458,#28459,#28460,#28461,#28462,#28463,#28464,#28465,#28466,#28467,
#28468,#28469,#28470,#28471,#28472,#28473,#28474,#28475,#28476,#28477)),
 .UNSPECIFIED.,.F.,.F.,.F.)
B_SPLINE_SURFACE_WITH_KNOTS((4,4),(3,2,2,2,2,2,2,2,2,2,2,2,2,2,2,2,2,2,
2,2,2,2,2,2,2,2,2,2,2,2,3),(0.,1.),(0.,0.0277777777777778,0.0555555555555556,
0.0833333333333333,0.111111111111111,0.138888888888889,0.166666666666667,
0.194444444444445,0.222222222222222,0.25,0.277777777777778,0.305555555555555,
0.333333333333334,0.361111111111111,0.388888888888889,0.416666666666667,
0.444444444444444,0.472222222222222,0.5,0.527777777777778,0.555555555555556,
0.583333333333333,0.611111111111111,0.638888888888889,0.666666666666667,
0.694444444444444,0.722222222222222,0.75,0.777777777777778,0.805555555555556,
0.833333333333333),.PIECEWISE_BEZIER_KNOTS.)
GEOMETRIC_REPRESENTATION_ITEM()
RATIONAL_B_SPLINE_SURFACE(((1.,0.965925826289068,1.,0.965925826289068,1.,
0.965925826289068,1.,0.965925826289068,1.,0.965925826289068,1.,0.965925826289068,
1.,0.965925826289068,1.,0.965925826289068,1.,0.965925826289068,1.,0.965925826289068,
1.,0.965925826289068,1.,0.965925826289068,1.,0.965925826289068,1.,0.965925826289068,
1.,0.965925826289068,1.,0.965925826289068,1.,0.965925826289068,1.,0.965925826289068,
1.,0.965925826289068,1.,0.965925826289068,1.,0.965925826289068,1.,0.965925826289068,
1.,0.965925826289068,1.,0.965925826289068,1.,0.965925826289068,1.,0.965925826289068,
1.,0.965925826289068,1.,0.965925826289068,1.,0.965925826289068,1.,0.965925826289068,
1.),(0.949253021674191,0.916908009318038,0.949253021674191,0.916908009318038,
0.949253021674191,0.916908009318038,0.949253021674191,0.916908009318038,
0.949253021674191,0.916908009318038,0.949253021674191,0.916908009318038,
0.949253021674191,0.916908009318038,0.949253021674191,0.916908009318038,
0.949253021674191,0.916908009318038,0.949253021674191,0.916908009318038,
0.949253021674191,0.916908009318038,0.949253021674191,0.916908009318038,
0.949253021674191,0.916908009318038,0.949253021674191,0.916908009318038,
0.949253021674191,0.916908009318038,0.949253021674191,0.916908009318038,
0.949253021674191,0.916908009318038,0.949253021674191,0.916908009318038,
0.949253021674191,0.916908009318038,0.949253021674191,0.916908009318038,
0.949253021674191,0.916908009318038,0.949253021674191,0.916908009318038,
0.949253021674191,0.916908009318038,0.949253021674191,0.916908009318038,
0.949253021674191,0.916908009318038,0.949253021674191,0.916908009318038,
0.949253021674191,0.916908009318038,0.949253021674191,0.916908009318038,
0.949253021674191,0.916908009318038,0.949253021674191,0.916908009318038,
0.949253021674191),(0.949253021674191,0.916908009318038,0.949253021674191,
0.916908009318038,0.949253021674191,0.916908009318038,0.949253021674191,
0.916908009318038,0.949253021674191,0.916908009318038,0.949253021674191,
0.916908009318038,0.949253021674191,0.916908009318038,0.949253021674191,
0.916908009318038,0.949253021674191,0.916908009318038,0.949253021674191,
0.916908009318038,0.949253021674191,0.916908009318038,0.949253021674191,
0.916908009318038,0.949253021674191,0.916908009318038,0.949253021674191,
0.916908009318038,0.949253021674191,0.916908009318038,0.949253021674191,
0.916908009318038,0.949253021674191,0.916908009318038,0.949253021674191,
0.916908009318038,0.949253021674191,0.916908009318038,0.949253021674191,
0.916908009318038,0.949253021674191,0.916908009318038,0.949253021674191,
0.916908009318038,0.949253021674191,0.916908009318038,0.949253021674191,
0.916908009318038,0.949253021674191,0.916908009318038,0.949253021674191,
0.916908009318038,0.949253021674191,0.916908009318038,0.949253021674191,
0.916908009318038,0.949253021674191,0.916908009318038,0.949253021674191,
0.916908009318038,0.949253021674191),(1.,0.965925826289068,1.,0.965925826289068,
1.,0.965925826289068,1.,0.965925826289068,1.,0.965925826289068,1.,0.965925826289068,
1.,0.965925826289068,1.,0.965925826289068,1.,0.965925826289068,1.,0.965925826289068,
1.,0.965925826289068,1.,0.965925826289068,1.,0.965925826289068,1.,0.965925826289068,
1.,0.965925826289068,1.,0.965925826289068,1.,0.965925826289068,1.,0.965925826289068,
1.,0.965925826289068,1.,0.965925826289068,1.,0.965925826289068,1.,0.965925826289068,
1.,0.965925826289068,1.,0.965925826289068,1.,0.965925826289068,1.,0.965925826289068,
1.,0.965925826289068,1.,0.965925826289068,1.,0.965925826289068,1.,0.965925826289068,
1.)))
REPRESENTATION_ITEM('')
SURFACE()
);
#12815=ADVANCED_FACE('',(#11744),#12668,.T.);
#12816=ADVANCED_FACE('',(#11745),#12669,.T.);
#12817=ADVANCED_FACE('',(#11746),#12670,.T.);
#12818=ADVANCED_FACE('',(#11747),#1576,.T.);
#12819=ADVANCED_FACE('',(#11748),#12671,.T.);
#12820=ADVANCED_FACE('',(#11749),#12672,.T.);
#12821=ADVANCED_FACE('',(#11750),#12673,.T.);
#12822=ADVANCED_FACE('',(#11751),#1237,.T.);
#12823=ADVANCED_FACE('',(#11752),#1238,.T.);
#12824=ADVANCED_FACE('',(#11753),#1239,.F.);
#12825=ADVANCED_FACE('',(#11754,#11755),#1577,.T.);
#13505=CLOSED_SHELL('',(#12815,#12816,#12817,#12818,#12819,#12820,#12821,
#12822,#12823,#12824,#12825));
#13532=STYLED_ITEM('',(#13559),#13722);
#13559=PRESENTATION_STYLE_ASSIGNMENT((#13586));
#13586=SURFACE_STYLE_USAGE(.BOTH.,#13613);
#13613=SURFACE_SIDE_STYLE('',(#13640));
#13640=SURFACE_STYLE_FILL_AREA(#13667);
#13667=FILL_AREA_STYLE('',(#13694));
#13694=FILL_AREA_STYLE_COLOUR('',#60);
#13722=MANIFOLD_SOLID_BREP('refill_cap',#13505);
#13750=SHAPE_DEFINITION_REPRESENTATION(#45530,#13778);
#13778=SHAPE_REPRESENTATION('refill_cap',(#13802),#45468);
#13802=AXIS2_PLACEMENT_3D('',#19109,#15295,#15296);
#13991=AXIS2_PLACEMENT_3D('',#27333,#15717,#15718);
#13992=AXIS2_PLACEMENT_3D('',#27721,#15720,#15721);
#13993=AXIS2_PLACEMENT_3D('',#27722,#15722,#15723);
#13994=AXIS2_PLACEMENT_3D('',#27774,#15724,#15725);
#13995=AXIS2_PLACEMENT_3D('',#28049,#15727,#15728);
#13996=AXIS2_PLACEMENT_3D('',#28498,#15730,#15731);
#13997=AXIS2_PLACEMENT_3D('',#28555,#15732,#15733);
#13998=AXIS2_PLACEMENT_3D('',#28557,#15735,#15736);
#13999=AXIS2_PLACEMENT_3D('',#28558,#15737,#15738);
#14000=AXIS2_PLACEMENT_3D('',#28559,#15739,#15740);
#14001=AXIS2_PLACEMENT_3D('',#28560,#15741,#15742);
#14002=AXIS2_PLACEMENT_3D('',#28562,#15743,#15744);
#15295=DIRECTION('',(0.,0.,1.));
#15296=DIRECTION('',(1.,0.,0.));
#15717=DIRECTION('',(2.2574675679014E-14,-1.,-2.69034508421066E-14));
#15718=DIRECTION('',(1.,0.,0.));
#15719=DIRECTION('',(-0.984807753012211,0.,0.173648177666916));
#15720=DIRECTION('',(2.73184799366419E-14,1.,-1.46992276411323E-27));
#15721=DIRECTION('',(-0.173648177667176,0.,-0.984807753012165));
#15722=DIRECTION('',(-4.56139972616518E-30,-5.72420986807231E-15,-1.));
#15723=DIRECTION('',(0.,1.,-5.72420986807231E-15));
#15724=DIRECTION('',(0.,0.,-1.));
#15725=DIRECTION('',(-1.,0.,0.));
#15726=DIRECTION('',(0.,9.91462232468849E-15,1.));
#15727=DIRECTION('',(0.,1.,0.));
#15728=DIRECTION('',(-1.,0.,5.46369598732789E-14));
#15729=DIRECTION('',(0.707106781186552,3.95413916520204E-15,0.707106781186544));
#15730=DIRECTION('',(-1.69409931513961E-14,-1.,1.69409931513985E-14));
#15731=DIRECTION('',(0.707106781186497,-2.2765399947205E-14,-0.707106781186598));
#15732=DIRECTION('',(0.,-1.,0.));
#15733=DIRECTION('',(1.,0.,0.));
#15734=DIRECTION('',(0.,0.,-1.));
#15735=DIRECTION('',(0.,0.,-1.));
#15736=DIRECTION('',(-1.,0.,0.));
#15737=DIRECTION('',(0.,0.,-1.));
#15738=DIRECTION('',(-1.,0.,0.));
#15739=DIRECTION('',(0.,0.,-1.));
#15740=DIRECTION('',(-1.,0.,0.));
#15741=DIRECTION('',(0.,0.,-1.));
#15742=DIRECTION('',(-1.,0.,0.));
#15743=DIRECTION('',(0.,0.,-1.));
#15744=DIRECTION('',(-1.,0.,0.));
#19109=CARTESIAN_POINT('',(0.,0.,0.));
#27051=CARTESIAN_POINT('',(-0.0175237463973022,0.0219318294183615,0.0829676293941348));
#27052=CARTESIAN_POINT('',(-0.0175118732224913,0.0219317957695828,0.0829683295255001));
#27053=CARTESIAN_POINT('',(-0.0175,0.0219317957695827,0.0829690291284178));
#27054=CARTESIAN_POINT('',(-0.0152548287001133,0.0219317957695827,0.0831013207950845));
#27055=CARTESIAN_POINT('',(-0.0133104533185637,0.0230543814195261,0.0832336124617511));
#27056=CARTESIAN_POINT('',(-0.0113660779370141,0.0241769670694694,0.0833659041284178));
#27057=CARTESIAN_POINT('',(-0.0102434922870708,0.0261213424510191,0.0834981957950845));
#27058=CARTESIAN_POINT('',(-0.00912090663712744,0.0280657178325686,0.0836304874617511));
#27059=CARTESIAN_POINT('',(-0.00912090663712744,0.0303108891324553,0.0837627791284178));
#27060=CARTESIAN_POINT('',(-0.00912090663712744,0.0325560604323421,0.0838950707950844));
#27061=CARTESIAN_POINT('',(-0.0102434922870708,0.0345004358138917,0.0840273624617511));
#27062=CARTESIAN_POINT('',(-0.0113660779370142,0.0364448111954412,0.0841596541284179));
#27063=CARTESIAN_POINT('',(-0.0133104533185638,0.0375673968453846,0.0842919457950845));
#27064=CARTESIAN_POINT('',(-0.0152548287001134,0.038689982495328,0.0844242374617512));
#27065=CARTESIAN_POINT('',(-0.0175,0.038689982495328,0.0845565291284178));
#27066=CARTESIAN_POINT('',(-0.0197451712998867,0.038689982495328,0.0846888207950845));
#27067=CARTESIAN_POINT('',(-0.0216895466814364,0.0375673968453846,0.0848211124617511));
#27068=CARTESIAN_POINT('',(-0.023633922062986,0.0364448111954412,0.0849534041284178));
#27069=CARTESIAN_POINT('',(-0.0247565077129293,0.0345004358138917,0.0850856957950845));
#27070=CARTESIAN_POINT('',(-0.0258790933628727,0.032556060432342,0.0852179874617511));
#27071=CARTESIAN_POINT('',(-0.0258790933628727,0.0303108891324553,0.0853502791284178));
#27072=CARTESIAN_POINT('',(-0.0258790933628727,0.0280657178325686,0.0854825707950845));
#27073=CARTESIAN_POINT('',(-0.0247565077129293,0.0261213424510191,0.0856148624617511));
#27074=CARTESIAN_POINT('',(-0.023633922062986,0.0241769670694694,0.0857471541284178));
#27075=CARTESIAN_POINT('',(-0.0216895466814364,0.0230543814195261,0.0858794457950845));
#27076=CARTESIAN_POINT('',(-0.0197451712998867,0.0219317957695827,0.0860117374617512));
#27077=CARTESIAN_POINT('',(-0.0175,0.0219317957695827,0.0861440291284178));
#27078=CARTESIAN_POINT('',(-0.0152548287001133,0.0219317957695827,0.0862763207950845));
#27079=CARTESIAN_POINT('',(-0.0133104533185637,0.0230543814195261,0.0864086124617511));
#27080=CARTESIAN_POINT('',(-0.0113660779370141,0.0241769670694694,0.0865409041284178));
#27081=CARTESIAN_POINT('',(-0.0102434922870708,0.0261213424510191,0.0866731957950845));
#27082=CARTESIAN_POINT('',(-0.00912090663712744,0.0280657178325686,0.0868054874617512));
#27083=CARTESIAN_POINT('',(-0.00912090663712744,0.0303108891324553,0.0869377791284178));
#27084=CARTESIAN_POINT('',(-0.00912090663712744,0.0325560604323421,0.0870700707950845));
#27085=CARTESIAN_POINT('',(-0.0102434922870708,0.0345004358138917,0.0872023624617511));
#27086=CARTESIAN_POINT('',(-0.0113660779370142,0.0364448111954412,0.0873346541284179));
#27087=CARTESIAN_POINT('',(-0.0133104533185638,0.0375673968453846,0.0874669457950845));
#27088=CARTESIAN_POINT('',(-0.0152548287001134,0.038689982495328,0.0875992374617512));
#27089=CARTESIAN_POINT('',(-0.0175,0.038689982495328,0.0877315291284178));
#27090=CARTESIAN_POINT('',(-0.0197451712998867,0.038689982495328,0.0878638207950845));
#27091=CARTESIAN_POINT('',(-0.0216895466814364,0.0375673968453846,0.0879961124617511));
#27092=CARTESIAN_POINT('',(-0.023633922062986,0.0364448111954412,0.0881284041284178));
#27093=CARTESIAN_POINT('',(-0.0247565077129293,0.0345004358138917,0.0882606957950845));
#27094=CARTESIAN_POINT('',(-0.0258790933628727,0.032556060432342,0.0883929874617511));
#27095=CARTESIAN_POINT('',(-0.0258790933628727,0.0303108891324553,0.0885252791284178));
#27096=CARTESIAN_POINT('',(-0.0175233864785942,0.0220588289083546,0.0829452358675848));
#27097=CARTESIAN_POINT('',(-0.017511693262776,0.0220587957695827,0.0829459359989501));
#27098=CARTESIAN_POINT('',(-0.0175,0.0220587957695827,0.0829466356018678));
#27099=CARTESIAN_POINT('',(-0.0152888582475521,0.0220587957695827,0.0830789272685345));
#27100=CARTESIAN_POINT('',(-0.0133739533185637,0.0231643666458067,0.0832112189352011));
#27101=CARTESIAN_POINT('',(-0.0114590483895754,0.0242699375220307,0.0833435106018678));
#27102=CARTESIAN_POINT('',(-0.0103534775133514,0.0261848424510191,0.0834758022685346));
#27103=CARTESIAN_POINT('',(-0.00924790663712745,0.0280997473800074,0.0836080939352012));
#27104=CARTESIAN_POINT('',(-0.00924790663712744,0.0303108891324553,0.0837403856018679));
#27105=CARTESIAN_POINT('',(-0.00924790663712745,0.0325220308849033,0.0838726772685345));
#27106=CARTESIAN_POINT('',(-0.0103534775133514,0.0344369358138917,0.0840049689352011));
#27107=CARTESIAN_POINT('',(-0.0114590483895754,0.03635184074288,0.0841372606018679));
#27108=CARTESIAN_POINT('',(-0.0133739533185638,0.037457411619104,0.0842695522685344));
#27109=CARTESIAN_POINT('',(-0.0152888582475521,0.0385629824953279,0.0844018439352012));
#27110=CARTESIAN_POINT('',(-0.0175,0.0385629824953279,0.0845341356018678));
#27111=CARTESIAN_POINT('',(-0.019711141752448,0.0385629824953279,0.0846664272685345));
#27112=CARTESIAN_POINT('',(-0.0216260466814364,0.037457411619104,0.0847987189352012));
#27113=CARTESIAN_POINT('',(-0.0235409516104247,0.03635184074288,0.0849310106018678));
#27114=CARTESIAN_POINT('',(-0.0246465224866487,0.0344369358138917,0.0850633022685345));
#27115=CARTESIAN_POINT('',(-0.0257520933628727,0.0325220308849033,0.0851955939352012));
#27116=CARTESIAN_POINT('',(-0.0257520933628727,0.0303108891324553,0.0853278856018678));
#27117=CARTESIAN_POINT('',(-0.0257520933628727,0.0280997473800074,0.0854601772685345));
#27118=CARTESIAN_POINT('',(-0.0246465224866487,0.026184842451019,0.0855924689352011));
#27119=CARTESIAN_POINT('',(-0.0235409516104247,0.0242699375220307,0.0857247606018678));
#27120=CARTESIAN_POINT('',(-0.0216260466814364,0.0231643666458067,0.0858570522685345));
#27121=CARTESIAN_POINT('',(-0.019711141752448,0.0220587957695827,0.0859893439352011));
#27122=CARTESIAN_POINT('',(-0.0175,0.0220587957695827,0.0861216356018678));
#27123=CARTESIAN_POINT('',(-0.0152888582475521,0.0220587957695827,0.0862539272685345));
#27124=CARTESIAN_POINT('',(-0.0133739533185637,0.0231643666458067,0.0863862189352011));
#27125=CARTESIAN_POINT('',(-0.0114590483895754,0.0242699375220307,0.0865185106018678));
#27126=CARTESIAN_POINT('',(-0.0103534775133514,0.0261848424510191,0.0866508022685344));
#27127=CARTESIAN_POINT('',(-0.00924790663712745,0.0280997473800074,0.0867830939352012));
#27128=CARTESIAN_POINT('',(-0.00924790663712744,0.0303108891324553,0.0869153856018678));
#27129=CARTESIAN_POINT('',(-0.00924790663712745,0.0325220308849033,0.0870476772685344));
#27130=CARTESIAN_POINT('',(-0.0103534775133514,0.0344369358138917,0.0871799689352011));
#27131=CARTESIAN_POINT('',(-0.0114590483895754,0.03635184074288,0.0873122606018678));
#27132=CARTESIAN_POINT('',(-0.0133739533185638,0.037457411619104,0.0874445522685345));
#27133=CARTESIAN_POINT('',(-0.0152888582475521,0.0385629824953279,0.0875768439352012));
#27134=CARTESIAN_POINT('',(-0.0175,0.0385629824953279,0.0877091356018679));
#27135=CARTESIAN_POINT('',(-0.019711141752448,0.0385629824953279,0.0878414272685345));
#27136=CARTESIAN_POINT('',(-0.0216260466814364,0.037457411619104,0.0879737189352012));
#27137=CARTESIAN_POINT('',(-0.0235409516104247,0.03635184074288,0.0881060106018679));
#27138=CARTESIAN_POINT('',(-0.0246465224866487,0.0344369358138917,0.0882383022685345));
#27139=CARTESIAN_POINT('',(-0.0257520933628727,0.0325220308849033,0.0883705939352012));
#27140=CARTESIAN_POINT('',(-0.0257520933628727,0.0303108891324553,0.0885028856018678));
#27141=CARTESIAN_POINT('',(-0.0175231515583417,0.0221417219383439,0.0828464474045792));
#27142=CARTESIAN_POINT('',(-0.0175115758024139,0.0221416891324553,0.0828471475359445));
#27143=CARTESIAN_POINT('',(-0.0175,0.0221416891324553,0.0828478471388622));
#27144=CARTESIAN_POINT('',(-0.0153110694571917,0.0221416891324553,0.0829801388055289));
#27145=CARTESIAN_POINT('',(-0.0134154,0.0232361544038595,0.0831124304721955));
#27146=CARTESIAN_POINT('',(-0.0115197305428084,0.0243306196752637,0.0832447221388622));
#27147=CARTESIAN_POINT('',(-0.0104252652714042,0.0262262891324553,0.0833770138055289));
#27148=CARTESIAN_POINT('',(-0.00933080000000003,0.028121958589647,0.0835093054721956));
#27149=CARTESIAN_POINT('',(-0.00933080000000004,0.0303108891324554,0.0836415971388622));
#27150=CARTESIAN_POINT('',(-0.00933080000000005,0.0324998196752637,0.0837738888055289));
#27151=CARTESIAN_POINT('',(-0.0104252652714042,0.0343954891324554,0.0839061804721955));
#27152=CARTESIAN_POINT('',(-0.0115197305428084,0.0362911585896471,0.0840384721388623));
#27153=CARTESIAN_POINT('',(-0.0134154000000001,0.0373856238610512,0.0841707638055288));
#27154=CARTESIAN_POINT('',(-0.0153110694571917,0.0384800891324554,0.0843030554721955));
#27155=CARTESIAN_POINT('',(-0.0175,0.0384800891324553,0.0844353471388622));
#27156=CARTESIAN_POINT('',(-0.0196889305428084,0.0384800891324554,0.0845676388055289));
#27157=CARTESIAN_POINT('',(-0.0215846,0.0373856238610511,0.0846999304721956));
#27158=CARTESIAN_POINT('',(-0.0234802694571917,0.036291158589647,0.0848322221388622));
#27159=CARTESIAN_POINT('',(-0.0245747347285959,0.0343954891324553,0.0849645138055289));
#27160=CARTESIAN_POINT('',(-0.0256692000000001,0.0324998196752637,0.0850968054721956));
#27161=CARTESIAN_POINT('',(-0.0256692,0.0303108891324553,0.0852290971388622));
#27162=CARTESIAN_POINT('',(-0.0256692000000001,0.028121958589647,0.0853613888055289));
#27163=CARTESIAN_POINT('',(-0.0245747347285959,0.0262262891324553,0.0854936804721955));
#27164=CARTESIAN_POINT('',(-0.0234802694571917,0.0243306196752637,0.0856259721388622));
#27165=CARTESIAN_POINT('',(-0.0215846,0.0232361544038595,0.0857582638055289));
#27166=CARTESIAN_POINT('',(-0.0196889305428084,0.0221416891324553,0.0858905554721955));
#27167=CARTESIAN_POINT('',(-0.0175,0.0221416891324553,0.0860228471388622));
#27168=CARTESIAN_POINT('',(-0.0153110694571917,0.0221416891324553,0.0861551388055289));
#27169=CARTESIAN_POINT('',(-0.0134154,0.0232361544038595,0.0862874304721955));
#27170=CARTESIAN_POINT('',(-0.0115197305428084,0.0243306196752637,0.0864197221388622));
#27171=CARTESIAN_POINT('',(-0.0104252652714042,0.0262262891324553,0.0865520138055288));
#27172=CARTESIAN_POINT('',(-0.00933080000000003,0.028121958589647,0.0866843054721956));
#27173=CARTESIAN_POINT('',(-0.00933080000000004,0.0303108891324554,0.0868165971388622));
#27174=CARTESIAN_POINT('',(-0.00933080000000005,0.0324998196752637,0.086948888805529));
#27175=CARTESIAN_POINT('',(-0.0104252652714042,0.0343954891324554,0.0870811804721955));
#27176=CARTESIAN_POINT('',(-0.0115197305428084,0.0362911585896471,0.0872134721388622));
#27177=CARTESIAN_POINT('',(-0.0134154000000001,0.0373856238610512,0.0873457638055289));
#27178=CARTESIAN_POINT('',(-0.0153110694571917,0.0384800891324554,0.0874780554721955));
#27179=CARTESIAN_POINT('',(-0.0175,0.0384800891324553,0.0876103471388623));
#27180=CARTESIAN_POINT('',(-0.0196889305428084,0.0384800891324554,0.0877426388055289));
#27181=CARTESIAN_POINT('',(-0.0215846,0.0373856238610511,0.0878749304721956));
#27182=CARTESIAN_POINT('',(-0.0234802694571917,0.036291158589647,0.0880072221388623));
#27183=CARTESIAN_POINT('',(-0.0245747347285959,0.0343954891324553,0.0881395138055289));
#27184=CARTESIAN_POINT('',(-0.0256692000000001,0.0324998196752637,0.0882718054721955));
#27185=CARTESIAN_POINT('',(-0.0256692,0.0303108891324553,0.0884040971388622));
#27186=CARTESIAN_POINT('',(-0.0175231515583417,0.0221417219383439,0.0827174882248697));
#27187=CARTESIAN_POINT('',(-0.0175115758024139,0.0221416891324554,0.082718188356235));
#27188=CARTESIAN_POINT('',(-0.0175,0.0221416891324554,0.0827188879591527));
#27189=CARTESIAN_POINT('',(-0.0153110694571917,0.0221416891324553,0.0828511796258194));
#27190=CARTESIAN_POINT('',(-0.0134154,0.0232361544038595,0.082983471292486));
#27191=CARTESIAN_POINT('',(-0.0115197305428084,0.0243306196752637,0.0831157629591527));
#27192=CARTESIAN_POINT('',(-0.0104252652714042,0.0262262891324554,0.0832480546258194));
#27193=CARTESIAN_POINT('',(-0.00933080000000004,0.028121958589647,0.083380346292486));
#27194=CARTESIAN_POINT('',(-0.0093308,0.0303108891324553,0.0835126379591527));
#27195=CARTESIAN_POINT('',(-0.00933080000000005,0.0324998196752637,0.0836449296258193));
#27196=CARTESIAN_POINT('',(-0.0104252652714042,0.0343954891324554,0.083777221292486));
#27197=CARTESIAN_POINT('',(-0.0115197305428084,0.0362911585896471,0.0839095129591528));
#27198=CARTESIAN_POINT('',(-0.0134154,0.0373856238610512,0.0840418046258194));
#27199=CARTESIAN_POINT('',(-0.0153110694571917,0.0384800891324554,0.0841740962924861));
#27200=CARTESIAN_POINT('',(-0.0175,0.0384800891324554,0.0843063879591527));
#27201=CARTESIAN_POINT('',(-0.0196889305428084,0.0384800891324553,0.0844386796258194));
#27202=CARTESIAN_POINT('',(-0.0215846,0.0373856238610511,0.084570971292486));
#27203=CARTESIAN_POINT('',(-0.0234802694571917,0.036291158589647,0.0847032629591527));
#27204=CARTESIAN_POINT('',(-0.0245747347285959,0.0343954891324554,0.0848355546258194));
#27205=CARTESIAN_POINT('',(-0.0256692000000001,0.0324998196752637,0.084967846292486));
#27206=CARTESIAN_POINT('',(-0.0256692,0.0303108891324553,0.0851001379591527));
#27207=CARTESIAN_POINT('',(-0.0256692000000001,0.028121958589647,0.0852324296258194));
#27208=CARTESIAN_POINT('',(-0.0245747347285959,0.0262262891324553,0.085364721292486));
#27209=CARTESIAN_POINT('',(-0.0234802694571917,0.0243306196752637,0.0854970129591527));
#27210=CARTESIAN_POINT('',(-0.0215846,0.0232361544038595,0.0856293046258194));
#27211=CARTESIAN_POINT('',(-0.0196889305428084,0.0221416891324553,0.0857615962924861));
#27212=CARTESIAN_POINT('',(-0.0175,0.0221416891324554,0.0858938879591527));
#27213=CARTESIAN_POINT('',(-0.0153110694571917,0.0221416891324553,0.0860261796258194));
#27214=CARTESIAN_POINT('',(-0.0134154,0.0232361544038595,0.086158471292486));
#27215=CARTESIAN_POINT('',(-0.0115197305428084,0.0243306196752637,0.0862907629591527));
#27216=CARTESIAN_POINT('',(-0.0104252652714042,0.0262262891324554,0.0864230546258194));
#27217=CARTESIAN_POINT('',(-0.00933080000000004,0.028121958589647,0.086555346292486));
#27218=CARTESIAN_POINT('',(-0.0093308,0.0303108891324553,0.0866876379591527));
#27219=CARTESIAN_POINT('',(-0.00933080000000005,0.0324998196752637,0.0868199296258194));
#27220=CARTESIAN_POINT('',(-0.0104252652714042,0.0343954891324554,0.086952221292486));
#27221=CARTESIAN_POINT('',(-0.0115197305428084,0.0362911585896471,0.0870845129591527));
#27222=CARTESIAN_POINT('',(-0.0134154,0.0373856238610512,0.0872168046258194));
#27223=CARTESIAN_POINT('',(-0.0153110694571917,0.0384800891324554,0.0873490962924861));
#27224=CARTESIAN_POINT('',(-0.0175,0.0384800891324554,0.0874813879591527));
#27225=CARTESIAN_POINT('',(-0.0196889305428084,0.0384800891324553,0.0876136796258194));
#27226=CARTESIAN_POINT('',(-0.0215846,0.0373856238610511,0.087745971292486));
#27227=CARTESIAN_POINT('',(-0.0234802694571917,0.036291158589647,0.0878782629591527));
#27228=CARTESIAN_POINT('',(-0.0245747347285959,0.0343954891324554,0.0880105546258194));
#27229=CARTESIAN_POINT('',(-0.0256692000000001,0.0324998196752637,0.088142846292486));
#27230=CARTESIAN_POINT('',(-0.0256692,0.0303108891324553,0.0882751379591527));
#27231=CARTESIAN_POINT('',(-0.0169787305804826,0.0219480257606184,0.0830000000000001));
#27232=CARTESIAN_POINT('',(-0.0150146757293008,0.022070448151928,0.083117660354341));
#27233=CARTESIAN_POINT('',(-0.0133104533185637,0.0230543814195261,0.0832336124617511));
#27234=CARTESIAN_POINT('',(-0.0113660779370141,0.0241769670694694,0.0833659041284178));
#27235=CARTESIAN_POINT('',(-0.0102434922870708,0.0261213424510191,0.0834981957950845));
#27236=CARTESIAN_POINT('',(-0.00912090663712744,0.0280657178325686,0.0836304874617511));
#27237=CARTESIAN_POINT('',(-0.00912090663712744,0.0303108891324553,0.0837627791284178));
#27238=CARTESIAN_POINT('',(-0.00912090663712745,0.0325560604323421,0.0838950707950844));
#27239=CARTESIAN_POINT('',(-0.0102434922870708,0.0345004358138917,0.0840273624617511));
#27240=CARTESIAN_POINT('',(-0.0113660779370142,0.0364448111954413,0.0841596541284179));
#27241=CARTESIAN_POINT('',(-0.0133104533185638,0.0375673968453846,0.0842919457950845));
#27242=CARTESIAN_POINT('',(-0.0152548287001134,0.038689982495328,0.0844242374617512));
#27243=CARTESIAN_POINT('',(-0.0175,0.038689982495328,0.0845565291284178));
#27244=CARTESIAN_POINT('',(-0.0197451712998867,0.038689982495328,0.0846888207950845));
#27245=CARTESIAN_POINT('',(-0.0216895466814364,0.0375673968453846,0.0848211124617511));
#27246=CARTESIAN_POINT('',(-0.023633922062986,0.0364448111954412,0.0849534041284178));
#27247=CARTESIAN_POINT('',(-0.0247565077129293,0.0345004358138917,0.0850856957950845));
#27248=CARTESIAN_POINT('',(-0.0258790933628727,0.032556060432342,0.0852179874617511));
#27249=CARTESIAN_POINT('',(-0.0258790933628727,0.0303108891324553,0.0853502791284178));
#27250=CARTESIAN_POINT('',(-0.0258790933628727,0.0280657178325686,0.0854825707950845));
#27251=CARTESIAN_POINT('',(-0.0247565077129293,0.026121342451019,0.0856148624617511));
#27252=CARTESIAN_POINT('',(-0.023633922062986,0.0241769670694694,0.0857471541284178));
#27253=CARTESIAN_POINT('',(-0.0216895466814364,0.0230543814195261,0.0858794457950845));
#27254=CARTESIAN_POINT('',(-0.0197451712998867,0.0219317957695827,0.0860117374617512));
#27255=CARTESIAN_POINT('',(-0.0175,0.0219317957695827,0.0861440291284178));
#27256=CARTESIAN_POINT('',(-0.0152548287001133,0.0219317957695827,0.0862763207950845));
#27257=CARTESIAN_POINT('',(-0.0133104533185637,0.0230543814195261,0.0864086124617511));
#27258=CARTESIAN_POINT('',(-0.0113660779370141,0.0241769670694694,0.0865409041284178));
#27259=CARTESIAN_POINT('',(-0.0102434922870708,0.0261213424510191,0.0866731957950845));
#27260=CARTESIAN_POINT('',(-0.00912090663712744,0.0280657178325686,0.0868054874617512));
#27261=CARTESIAN_POINT('',(-0.00912090663712744,0.0303108891324553,0.0869377791284178));
#27262=CARTESIAN_POINT('',(-0.00912090663712745,0.0325560604323421,0.0870700707950845));
#27263=CARTESIAN_POINT('',(-0.0102434922870708,0.0345004358138917,0.0872023624617511));
#27264=CARTESIAN_POINT('',(-0.0113660779370142,0.0364448111954413,0.0873346541284178));
#27265=CARTESIAN_POINT('',(-0.0133104533185638,0.0375673968453846,0.0874669457950845));
#27266=CARTESIAN_POINT('',(-0.0152548287001134,0.038689982495328,0.0875992374617512));
#27267=CARTESIAN_POINT('',(-0.0175,0.038689982495328,0.0877315291284178));
#27268=CARTESIAN_POINT('',(-0.0197451712998867,0.038689982495328,0.0878638207950845));
#27269=CARTESIAN_POINT('',(-0.0216895466814364,0.0375673968453846,0.0879961124617511));
#27270=CARTESIAN_POINT('',(-0.023633922062986,0.0364448111954412,0.0881284041284178));
#27271=CARTESIAN_POINT('',(-0.0247565077129293,0.0345004358138917,0.0882606957950845));
#27272=CARTESIAN_POINT('',(-0.0258790933628727,0.032556060432342,0.0883929874617511));
#27273=CARTESIAN_POINT('',(-0.0258790933628727,0.0303108891324553,0.0885252791284178));
#27274=CARTESIAN_POINT('',(-0.0169787305804826,0.0219480257606184,0.083));
#27275=CARTESIAN_POINT('',(-0.0258790933628727,0.0303108891324553,0.0885252791284178));
#27276=CARTESIAN_POINT('',(-0.0169787305804826,0.0219480257606184,0.083));
#27277=CARTESIAN_POINT('',(-0.0168200873191828,0.0220130837286955,0.083));
#27278=CARTESIAN_POINT('',(-0.0164839350506513,0.0220712803175494,0.0829999999999999));
#27279=CARTESIAN_POINT('',(-0.0158244416844979,0.0222361631417369,0.0830000000000002));
#27280=CARTESIAN_POINT('',(-0.0150115364146986,0.0224757860232567,0.0829999999999978));
#27281=CARTESIAN_POINT('',(-0.0140666789792818,0.0228698014663725,0.0830000000000006));
#27282=CARTESIAN_POINT('',(-0.0134711325811131,0.0231961039553641,0.083));
#27283=CARTESIAN_POINT('',(-0.0131818748312345,0.0233762208875518,0.083));
#27284=CARTESIAN_POINT('',(-0.0131818748312345,0.0233762208875518,0.083));
#27285=CARTESIAN_POINT('',(-0.0131818748312345,0.0233762208875518,0.083));
#27286=CARTESIAN_POINT('',(-0.0114470797111507,0.0244564546069068,0.0831245445074173));
#27287=CARTESIAN_POINT('',(-0.0104252652714042,0.0262262891324554,0.0832480546258194));
#27288=CARTESIAN_POINT('',(-0.00933080000000005,0.028121958589647,0.0833803462924859));
#27289=CARTESIAN_POINT('',(-0.0093308,0.0303108891324553,0.0835126379591527));
#27290=CARTESIAN_POINT('',(-0.0093308,0.0303108891324553,0.0835126379591527));
#27291=CARTESIAN_POINT('',(-0.0093308,0.0303108891324553,0.0835126379591527));
#27292=CARTESIAN_POINT('',(-0.00933080000000004,0.0324998196752637,0.0836449296258193));
#27293=CARTESIAN_POINT('',(-0.0104252652714042,0.0343954891324554,0.083777221292486));
#27294=CARTESIAN_POINT('',(-0.0115197305428084,0.0362911585896471,0.0839095129591528));
#27295=CARTESIAN_POINT('',(-0.0134154,0.0373856238610512,0.0840418046258194));
#27296=CARTESIAN_POINT('',(-0.0153110694571917,0.0384800891324554,0.0841740962924861));
#27297=CARTESIAN_POINT('',(-0.0175,0.0384800891324554,0.0843063879591527));
#27298=CARTESIAN_POINT('',(-0.0196889305428084,0.0384800891324553,0.0844386796258194));
#27299=CARTESIAN_POINT('',(-0.0215846,0.0373856238610511,0.084570971292486));
#27300=CARTESIAN_POINT('',(-0.0234802694571917,0.036291158589647,0.0847032629591527));
#27301=CARTESIAN_POINT('',(-0.0245747347285959,0.0343954891324554,0.0848355546258194));
#27302=CARTESIAN_POINT('',(-0.0256692000000001,0.0324998196752637,0.084967846292486));
#27303=CARTESIAN_POINT('',(-0.0256692,0.0303108891324553,0.0851001379591527));
#27304=CARTESIAN_POINT('',(-0.0256692,0.0303108891324553,0.0851001379591527));
#27305=CARTESIAN_POINT('',(-0.0256692,0.0303108891324553,0.0851001379591527));
#27306=CARTESIAN_POINT('',(-0.0256692,0.028121958589647,0.0852324296258194));
#27307=CARTESIAN_POINT('',(-0.0245747347285959,0.0262262891324553,0.085364721292486));
#27308=CARTESIAN_POINT('',(-0.0234802694571917,0.0243306196752637,0.0854970129591527));
#27309=CARTESIAN_POINT('',(-0.0215846,0.0232361544038595,0.0856293046258194));
#27310=CARTESIAN_POINT('',(-0.0196889305428084,0.0221416891324553,0.0857615962924861));
#27311=CARTESIAN_POINT('',(-0.0175,0.0221416891324554,0.0858938879591527));
#27312=CARTESIAN_POINT('',(-0.0153110694571917,0.0221416891324553,0.0860261796258194));
#27313=CARTESIAN_POINT('',(-0.0134154,0.0232361544038595,0.086158471292486));
#27314=CARTESIAN_POINT('',(-0.0115197305428084,0.0243306196752637,0.0862907629591527));
#27315=CARTESIAN_POINT('',(-0.0104252652714042,0.0262262891324554,0.0864230546258194));
#27316=CARTESIAN_POINT('',(-0.00933080000000006,0.028121958589647,0.0865553462924861));
#27317=CARTESIAN_POINT('',(-0.0093308,0.0303108891324553,0.0866876379591526));
#27318=CARTESIAN_POINT('',(-0.0093308,0.0303108891324553,0.0866876379591527));
#27319=CARTESIAN_POINT('',(-0.0093308,0.0303108891324553,0.0866876379591527));
#27320=CARTESIAN_POINT('',(-0.00933080000000003,0.0324998196752637,0.0868199296258194));
#27321=CARTESIAN_POINT('',(-0.0104252652714042,0.0343954891324554,0.086952221292486));
#27322=CARTESIAN_POINT('',(-0.0115197305428084,0.0362911585896471,0.0870845129591527));
#27323=CARTESIAN_POINT('',(-0.0134154,0.0373856238610512,0.0872168046258194));
#27324=CARTESIAN_POINT('',(-0.0153110694571917,0.0384800891324554,0.0873490962924861));
#27325=CARTESIAN_POINT('',(-0.0175,0.0384800891324554,0.0874813879591527));
#27326=CARTESIAN_POINT('',(-0.0196889305428084,0.0384800891324553,0.0876136796258194));
#27327=CARTESIAN_POINT('',(-0.0215846,0.0373856238610511,0.087745971292486));
#27328=CARTESIAN_POINT('',(-0.0234802694571917,0.036291158589647,0.0878782629591527));
#27329=CARTESIAN_POINT('',(-0.0245747347285959,0.0343954891324554,0.0880105546258194));
#27330=CARTESIAN_POINT('',(-0.0256692000000001,0.0324998196752637,0.088142846292486));
#27331=CARTESIAN_POINT('',(-0.0256692,0.0303108891324553,0.0882751379591527));
#27332=CARTESIAN_POINT('',(-0.0256692,0.0303108891324553,0.0882751379591527));
#27333=CARTESIAN_POINT('',(-0.0259232,0.0303108891324553,0.0882751379591527));
#27334=CARTESIAN_POINT('',(-0.019581657813752,0.0215281047350537,0.0829656841085059));
#27335=CARTESIAN_POINT('',(-0.0185550497149152,0.0212847824953279,0.0830254048361197));
#27336=CARTESIAN_POINT('',(-0.0175,0.021284782495328,0.0830831150255454));
#27337=CARTESIAN_POINT('',(-0.0150814620157846,0.021284782495328,0.0832154066922121));
#27338=CARTESIAN_POINT('',(-0.0129869466814363,0.0224940514874357,0.0833476983588788));
#27339=CARTESIAN_POINT('',(-0.0108924313470881,0.0237033204795435,0.0834799900255455));
#27340=CARTESIAN_POINT('',(-0.00968316235498038,0.0257978358138917,0.0836122816922121));
#27341=CARTESIAN_POINT('',(-0.00847389336287265,0.0278923511482399,0.0837445733588788));
#27342=CARTESIAN_POINT('',(-0.00847389336287264,0.0303108891324553,0.0838768650255454));
#27343=CARTESIAN_POINT('',(-0.00847389336287266,0.0327294271166709,0.0840091566922122));
#27344=CARTESIAN_POINT('',(-0.00968316235498039,0.0348239424510191,0.0841414483588788));
#27345=CARTESIAN_POINT('',(-0.0108924313470881,0.0369184577853673,0.0842737400255455));
#27346=CARTESIAN_POINT('',(-0.0129869466814364,0.038127726777475,0.0844060316922121));
#27347=CARTESIAN_POINT('',(-0.0150814620157846,0.0393369957695828,0.0845383233588788));
#27348=CARTESIAN_POINT('',(-0.0175,0.0393369957695828,0.0846706150255454));
#27349=CARTESIAN_POINT('',(-0.0199185379842156,0.0393369957695828,0.0848029066922121));
#27350=CARTESIAN_POINT('',(-0.0220130533185638,0.038127726777475,0.0849351983588788));
#27351=CARTESIAN_POINT('',(-0.024107568652912,0.0369184577853673,0.0850674900255454));
#27352=CARTESIAN_POINT('',(-0.0253168376450197,0.0348239424510191,0.0851997816922121));
#27353=CARTESIAN_POINT('',(-0.0265261066371274,0.0327294271166708,0.0853320733588788));
#27354=CARTESIAN_POINT('',(-0.0265261066371274,0.0303108891324553,0.0854643650255454));
#27355=CARTESIAN_POINT('',(-0.0265261066371274,0.0278923511482398,0.0855966566922121));
#27356=CARTESIAN_POINT('',(-0.0253168376450197,0.0257978358138916,0.0857289483588788));
#27357=CARTESIAN_POINT('',(-0.024107568652912,0.0237033204795434,0.0858612400255455));
#27358=CARTESIAN_POINT('',(-0.0220130533185638,0.0224940514874356,0.0859935316922121));
#27359=CARTESIAN_POINT('',(-0.0199185379842155,0.0212847824953279,0.0861258233588788));
#27360=CARTESIAN_POINT('',(-0.0175,0.021284782495328,0.0862581150255454));
#27361=CARTESIAN_POINT('',(-0.0150814620157846,0.021284782495328,0.0863904066922121));
#27362=CARTESIAN_POINT('',(-0.0129869466814363,0.0224940514874357,0.0865226983588788));
#27363=CARTESIAN_POINT('',(-0.0108924313470881,0.0237033204795435,0.0866549900255455));
#27364=CARTESIAN_POINT('',(-0.00968316235498038,0.0257978358138917,0.0867872816922121));
#27365=CARTESIAN_POINT('',(-0.00847389336287265,0.0278923511482399,0.0869195733588788));
#27366=CARTESIAN_POINT('',(-0.00847389336287264,0.0303108891324553,0.0870518650255454));
#27367=CARTESIAN_POINT('',(-0.00847389336287266,0.0327294271166709,0.0871841566922122));
#27368=CARTESIAN_POINT('',(-0.00968316235498039,0.0348239424510191,0.0873164483588788));
#27369=CARTESIAN_POINT('',(-0.0108924313470881,0.0369184577853673,0.0874487400255455));
#27370=CARTESIAN_POINT('',(-0.0129869466814364,0.038127726777475,0.0875810316922121));
#27371=CARTESIAN_POINT('',(-0.0150814620157846,0.0393369957695828,0.0877133233588788));
#27372=CARTESIAN_POINT('',(-0.0175,0.0393369957695828,0.0878456150255454));
#27373=CARTESIAN_POINT('',(-0.0199185379842156,0.0393369957695828,0.0879779066922121));
#27374=CARTESIAN_POINT('',(-0.0220130533185638,0.038127726777475,0.0881101983588788));
#27375=CARTESIAN_POINT('',(-0.024107568652912,0.0369184577853673,0.0882424900255454));
#27376=CARTESIAN_POINT('',(-0.0253168376450197,0.0348239424510191,0.0883747816922121));
#27377=CARTESIAN_POINT('',(-0.0265261066371274,0.0327294271166708,0.0885070733588787));
#27378=CARTESIAN_POINT('',(-0.0265261066371274,0.0303108891324553,0.0886393650255454));
#27379=CARTESIAN_POINT('',(-0.0194324395192978,0.0221576760794319,0.0828515982113783));
#27380=CARTESIAN_POINT('',(-0.0184794211855844,0.0219317957695827,0.0829113189389921));
#27381=CARTESIAN_POINT('',(-0.0175,0.0219317957695827,0.0829690291284178));
#27382=CARTESIAN_POINT('',(-0.0152548287001133,0.0219317957695827,0.0831013207950845));
#27383=CARTESIAN_POINT('',(-0.0133104533185637,0.0230543814195261,0.0832336124617511));
#27384=CARTESIAN_POINT('',(-0.0113660779370141,0.0241769670694694,0.0833659041284178));
#27385=CARTESIAN_POINT('',(-0.0102434922870708,0.0261213424510191,0.0834981957950845));
#27386=CARTESIAN_POINT('',(-0.00912090663712744,0.0280657178325686,0.0836304874617511));
#27387=CARTESIAN_POINT('',(-0.00912090663712744,0.0303108891324553,0.0837627791284178));
#27388=CARTESIAN_POINT('',(-0.00912090663712745,0.0325560604323421,0.0838950707950844));
#27389=CARTESIAN_POINT('',(-0.0102434922870708,0.0345004358138917,0.0840273624617511));
#27390=CARTESIAN_POINT('',(-0.0113660779370142,0.0364448111954413,0.0841596541284179));
#27391=CARTESIAN_POINT('',(-0.0133104533185638,0.0375673968453846,0.0842919457950845));
#27392=CARTESIAN_POINT('',(-0.0152548287001134,0.038689982495328,0.0844242374617512));
#27393=CARTESIAN_POINT('',(-0.0175,0.038689982495328,0.0845565291284178));
#27394=CARTESIAN_POINT('',(-0.0197451712998867,0.038689982495328,0.0846888207950845));
#27395=CARTESIAN_POINT('',(-0.0216895466814364,0.0375673968453846,0.0848211124617511));
#27396=CARTESIAN_POINT('',(-0.023633922062986,0.0364448111954412,0.0849534041284178));
#27397=CARTESIAN_POINT('',(-0.0247565077129293,0.0345004358138917,0.0850856957950845));
#27398=CARTESIAN_POINT('',(-0.0258790933628727,0.032556060432342,0.0852179874617511));
#27399=CARTESIAN_POINT('',(-0.0258790933628727,0.0303108891324553,0.0853502791284178));
#27400=CARTESIAN_POINT('',(-0.0258790933628727,0.0280657178325686,0.0854825707950845));
#27401=CARTESIAN_POINT('',(-0.0247565077129293,0.026121342451019,0.0856148624617511));
#27402=CARTESIAN_POINT('',(-0.023633922062986,0.0241769670694694,0.0857471541284178));
#27403=CARTESIAN_POINT('',(-0.0216895466814364,0.0230543814195261,0.0858794457950845));
#27404=CARTESIAN_POINT('',(-0.0197451712998867,0.0219317957695827,0.0860117374617512));
#27405=CARTESIAN_POINT('',(-0.0175,0.0219317957695827,0.0861440291284178));
#27406=CARTESIAN_POINT('',(-0.0152548287001133,0.0219317957695827,0.0862763207950845));
#27407=CARTESIAN_POINT('',(-0.0133104533185637,0.0230543814195261,0.0864086124617511));
#27408=CARTESIAN_POINT('',(-0.0113660779370141,0.0241769670694694,0.0865409041284178));
#27409=CARTESIAN_POINT('',(-0.0102434922870708,0.0261213424510191,0.0866731957950845));
#27410=CARTESIAN_POINT('',(-0.00912090663712744,0.0280657178325686,0.0868054874617512));
#27411=CARTESIAN_POINT('',(-0.00912090663712744,0.0303108891324553,0.0869377791284178));
#27412=CARTESIAN_POINT('',(-0.00912090663712745,0.0325560604323421,0.0870700707950845));
#27413=CARTESIAN_POINT('',(-0.0102434922870708,0.0345004358138917,0.0872023624617511));
#27414=CARTESIAN_POINT('',(-0.0113660779370142,0.0364448111954413,0.0873346541284179));
#27415=CARTESIAN_POINT('',(-0.0133104533185638,0.0375673968453846,0.0874669457950845));
#27416=CARTESIAN_POINT('',(-0.0152548287001134,0.038689982495328,0.0875992374617512));
#27417=CARTESIAN_POINT('',(-0.0175,0.038689982495328,0.0877315291284178));
#27418=CARTESIAN_POINT('',(-0.0197451712998867,0.038689982495328,0.0878638207950845));
#27419=CARTESIAN_POINT('',(-0.0216895466814364,0.0375673968453846,0.0879961124617511));
#27420=CARTESIAN_POINT('',(-0.023633922062986,0.0364448111954412,0.0881284041284178));
#27421=CARTESIAN_POINT('',(-0.0247565077129293,0.0345004358138917,0.0882606957950845));
#27422=CARTESIAN_POINT('',(-0.0258790933628727,0.032556060432342,0.0883929874617511));
#27423=CARTESIAN_POINT('',(-0.0258790933628727,0.0303108891324553,0.0885252791284178));
#27424=CARTESIAN_POINT('',(-0.0189864747528493,0.0214080247712547,0.083));
#27425=CARTESIAN_POINT('',(-0.0182483463291824,0.0212847824953279,0.0830421812119037));
#27426=CARTESIAN_POINT('',(-0.0175,0.021284782495328,0.0830831150255454));
#27427=CARTESIAN_POINT('',(-0.0150814620157846,0.021284782495328,0.0832154066922121));
#27428=CARTESIAN_POINT('',(-0.0129869466814363,0.0224940514874357,0.0833476983588788));
#27429=CARTESIAN_POINT('',(-0.0108924313470881,0.0237033204795435,0.0834799900255455));
#27430=CARTESIAN_POINT('',(-0.00968316235498038,0.0257978358138917,0.0836122816922121));
#27431=CARTESIAN_POINT('',(-0.00847389336287265,0.0278923511482399,0.0837445733588788));
#27432=CARTESIAN_POINT('',(-0.00847389336287265,0.0303108891324553,0.0838768650255454));
#27433=CARTESIAN_POINT('',(-0.00847389336287266,0.0327294271166709,0.0840091566922122));
#27434=CARTESIAN_POINT('',(-0.00968316235498039,0.0348239424510191,0.0841414483588788));
#27435=CARTESIAN_POINT('',(-0.0108924313470881,0.0369184577853673,0.0842737400255455));
#27436=CARTESIAN_POINT('',(-0.0129869466814364,0.038127726777475,0.0844060316922121));
#27437=CARTESIAN_POINT('',(-0.0150814620157846,0.0393369957695828,0.0845383233588788));
#27438=CARTESIAN_POINT('',(-0.0175,0.0393369957695828,0.0846706150255454));
#27439=CARTESIAN_POINT('',(-0.0199185379842156,0.0393369957695828,0.0848029066922121));
#27440=CARTESIAN_POINT('',(-0.0220130533185638,0.038127726777475,0.0849351983588788));
#27441=CARTESIAN_POINT('',(-0.024107568652912,0.0369184577853673,0.0850674900255454));
#27442=CARTESIAN_POINT('',(-0.0253168376450197,0.0348239424510191,0.0851997816922121));
#27443=CARTESIAN_POINT('',(-0.0265261066371274,0.0327294271166708,0.0853320733588788));
#27444=CARTESIAN_POINT('',(-0.0265261066371274,0.0303108891324553,0.0854643650255454));
#27445=CARTESIAN_POINT('',(-0.0265261066371274,0.0278923511482398,0.0855966566922121));
#27446=CARTESIAN_POINT('',(-0.0253168376450197,0.0257978358138916,0.0857289483588788));
#27447=CARTESIAN_POINT('',(-0.0241075686529119,0.0237033204795434,0.0858612400255455));
#27448=CARTESIAN_POINT('',(-0.0220130533185638,0.0224940514874356,0.0859935316922121));
#27449=CARTESIAN_POINT('',(-0.0199185379842155,0.021284782495328,0.0861258233588788));
#27450=CARTESIAN_POINT('',(-0.0175,0.021284782495328,0.0862581150255454));
#27451=CARTESIAN_POINT('',(-0.0150814620157846,0.021284782495328,0.0863904066922121));
#27452=CARTESIAN_POINT('',(-0.0129869466814363,0.0224940514874357,0.0865226983588788));
#27453=CARTESIAN_POINT('',(-0.0108924313470881,0.0237033204795435,0.0866549900255454));
#27454=CARTESIAN_POINT('',(-0.00968316235498038,0.0257978358138917,0.0867872816922121));
#27455=CARTESIAN_POINT('',(-0.00847389336287265,0.0278923511482399,0.0869195733588788));
#27456=CARTESIAN_POINT('',(-0.00847389336287265,0.0303108891324553,0.0870518650255454));
#27457=CARTESIAN_POINT('',(-0.00847389336287266,0.0327294271166709,0.0871841566922122));
#27458=CARTESIAN_POINT('',(-0.00968316235498039,0.0348239424510191,0.0873164483588788));
#27459=CARTESIAN_POINT('',(-0.0108924313470881,0.0369184577853673,0.0874487400255455));
#27460=CARTESIAN_POINT('',(-0.0129869466814364,0.038127726777475,0.0875810316922121));
#27461=CARTESIAN_POINT('',(-0.0150814620157846,0.0393369957695828,0.0877133233588788));
#27462=CARTESIAN_POINT('',(-0.0175,0.0393369957695828,0.0878456150255454));
#27463=CARTESIAN_POINT('',(-0.0199185379842156,0.0393369957695828,0.0879779066922121));
#27464=CARTESIAN_POINT('',(-0.0220130533185638,0.038127726777475,0.0881101983588788));
#27465=CARTESIAN_POINT('',(-0.024107568652912,0.0369184577853673,0.0882424900255454));
#27466=CARTESIAN_POINT('',(-0.0253168376450197,0.0348239424510191,0.0883747816922121));
#27467=CARTESIAN_POINT('',(-0.0265261066371274,0.0327294271166708,0.0885070733588787));
#27468=CARTESIAN_POINT('',(-0.0265261066371274,0.0303108891324553,0.0886393650255454));
#27469=CARTESIAN_POINT('',(-0.0189864747528493,0.0214080247712546,0.083));
#27470=CARTESIAN_POINT('',(-0.0265261066371274,0.0303108891324553,0.0886393650255454));
#27471=CARTESIAN_POINT('',(-0.0189864747528493,0.0214080247712546,0.083));
#27472=CARTESIAN_POINT('',(-0.0182985666809634,0.0215077465167656,0.083));
#27473=CARTESIAN_POINT('',(-0.0176219168655072,0.0216842616873385,0.083));
#27474=CARTESIAN_POINT('',(-0.0169787305804826,0.0219480257606184,0.083));
#27475=CARTESIAN_POINT('',(-0.0262026,0.0303108891324553,0.0885823220769816));
#27476=CARTESIAN_POINT('',(-0.0236647323997788,0.023433406276125,0.0829642728854406));
#27477=CARTESIAN_POINT('',(-0.0229496504750082,0.0227924321287199,0.0830173387180816));
#27478=CARTESIAN_POINT('',(-0.022118,0.0223122785031023,0.0830686728614772));
#27479=CARTESIAN_POINT('',(-0.0199747787412939,0.0210748891324553,0.0832009645281439));
#27480=CARTESIAN_POINT('',(-0.0175,0.0210748891324553,0.0833332561948105));
#27481=CARTESIAN_POINT('',(-0.0150252212587062,0.0210748891324553,0.0834655478614772));
#27482=CARTESIAN_POINT('',(-0.012882,0.0223122785031023,0.0835978395281439));
#27483=CARTESIAN_POINT('',(-0.0107387787412939,0.0235496678737492,0.0837301311948106));
#27484=CARTESIAN_POINT('',(-0.00950138937064696,0.0256928891324554,0.0838624228614772));
#27485=CARTESIAN_POINT('',(-0.00826400000000004,0.0278361103911615,0.0839947145281439));
#27486=CARTESIAN_POINT('',(-0.008264,0.0303108891324553,0.0841270061948105));
#27487=CARTESIAN_POINT('',(-0.00826400000000004,0.0327856678737492,0.0842592978614772));
#27488=CARTESIAN_POINT('',(-0.00950138937064697,0.0349288891324553,0.0843915895281439));
#27489=CARTESIAN_POINT('',(-0.0107387787412939,0.0370721103911615,0.0845238811948106));
#27490=CARTESIAN_POINT('',(-0.012882,0.0383094997618084,0.0846561728614772));
#27491=CARTESIAN_POINT('',(-0.0150252212587062,0.0395468891324554,0.0847884645281439));
#27492=CARTESIAN_POINT('',(-0.0175,0.0395468891324554,0.0849207561948105));
#27493=CARTESIAN_POINT('',(-0.0199747787412939,0.0395468891324554,0.0850530478614772));
#27494=CARTESIAN_POINT('',(-0.022118,0.0383094997618084,0.0851853395281439));
#27495=CARTESIAN_POINT('',(-0.0242612212587062,0.0370721103911615,0.0853176311948106));
#27496=CARTESIAN_POINT('',(-0.0254986106293531,0.0349288891324553,0.0854499228614772));
#27497=CARTESIAN_POINT('',(-0.0267360000000001,0.0327856678737492,0.0855822145281439));
#27498=CARTESIAN_POINT('',(-0.026736,0.0303108891324553,0.0857145061948105));
#27499=CARTESIAN_POINT('',(-0.0267360000000001,0.0278361103911615,0.0858467978614772));
#27500=CARTESIAN_POINT('',(-0.0254986106293531,0.0256928891324553,0.0859790895281439));
#27501=CARTESIAN_POINT('',(-0.0242612212587062,0.0235496678737492,0.0861113811948106));
#27502=CARTESIAN_POINT('',(-0.022118,0.0223122785031023,0.0862436728614772));
#27503=CARTESIAN_POINT('',(-0.0199747787412939,0.0210748891324553,0.0863759645281439));
#27504=CARTESIAN_POINT('',(-0.0175,0.0210748891324553,0.0865082561948105));
#27505=CARTESIAN_POINT('',(-0.0150252212587062,0.0210748891324553,0.0866405478614773));
#27506=CARTESIAN_POINT('',(-0.012882,0.0223122785031023,0.0867728395281439));
#27507=CARTESIAN_POINT('',(-0.0107387787412939,0.0235496678737492,0.0869051311948106));
#27508=CARTESIAN_POINT('',(-0.00950138937064696,0.0256928891324554,0.0870374228614772));
#27509=CARTESIAN_POINT('',(-0.00826400000000004,0.0278361103911615,0.0871697145281439));
#27510=CARTESIAN_POINT('',(-0.008264,0.0303108891324553,0.0873020061948105));
#27511=CARTESIAN_POINT('',(-0.00826400000000004,0.0327856678737492,0.0874342978614772));
#27512=CARTESIAN_POINT('',(-0.00950138937064697,0.0349288891324553,0.0875665895281439));
#27513=CARTESIAN_POINT('',(-0.0107387787412939,0.0370721103911615,0.0876988811948106));
#27514=CARTESIAN_POINT('',(-0.012882,0.0383094997618084,0.0878311728614772));
#27515=CARTESIAN_POINT('',(-0.0150252212587062,0.0395468891324554,0.0879634645281439));
#27516=CARTESIAN_POINT('',(-0.0175,0.0395468891324554,0.0880957561948105));
#27517=CARTESIAN_POINT('',(-0.0199747787412939,0.0395468891324554,0.0882280478614772));
#27518=CARTESIAN_POINT('',(-0.022118,0.0383094997618084,0.0883603395281439));
#27519=CARTESIAN_POINT('',(-0.0242612212587062,0.0370721103911615,0.0884926311948105));
#27520=CARTESIAN_POINT('',(-0.0254986106293531,0.0349288891324553,0.0886249228614772));
#27521=CARTESIAN_POINT('',(-0.0267360000000001,0.0327856678737492,0.0887572145281438));
#27522=CARTESIAN_POINT('',(-0.026736,0.0303108891324553,0.0888895061948105));
#27523=CARTESIAN_POINT('',(-0.0236647323997788,0.023433406276125,0.0828353137057312));
#27524=CARTESIAN_POINT('',(-0.0229496504750083,0.0227924321287199,0.0828883795383722));
#27525=CARTESIAN_POINT('',(-0.022118,0.0223122785031023,0.0829397136817678));
#27526=CARTESIAN_POINT('',(-0.0199747787412939,0.0210748891324553,0.0830720053484343));
#27527=CARTESIAN_POINT('',(-0.0175,0.0210748891324553,0.083204297015101));
#27528=CARTESIAN_POINT('',(-0.0150252212587062,0.0210748891324553,0.0833365886817677));
#27529=CARTESIAN_POINT('',(-0.012882,0.0223122785031023,0.0834688803484343));
#27530=CARTESIAN_POINT('',(-0.0107387787412939,0.0235496678737492,0.0836011720151011));
#27531=CARTESIAN_POINT('',(-0.00950138937064695,0.0256928891324553,0.0837334636817677));
#27532=CARTESIAN_POINT('',(-0.00826400000000004,0.0278361103911615,0.0838657553484344));
#27533=CARTESIAN_POINT('',(-0.00826400000000004,0.0303108891324553,0.0839980470151011));
#27534=CARTESIAN_POINT('',(-0.00826400000000004,0.0327856678737492,0.0841303386817678));
#27535=CARTESIAN_POINT('',(-0.00950138937064697,0.0349288891324553,0.0842626303484344));
#27536=CARTESIAN_POINT('',(-0.0107387787412939,0.0370721103911615,0.084394922015101));
#27537=CARTESIAN_POINT('',(-0.0128820000000001,0.0383094997618084,0.0845272136817677));
#27538=CARTESIAN_POINT('',(-0.0150252212587062,0.0395468891324554,0.0846595053484344));
#27539=CARTESIAN_POINT('',(-0.0175000000000001,0.0395468891324553,0.084791797015101));
#27540=CARTESIAN_POINT('',(-0.0199747787412939,0.0395468891324554,0.0849240886817677));
#27541=CARTESIAN_POINT('',(-0.0221180000000001,0.0383094997618084,0.0850563803484344));
#27542=CARTESIAN_POINT('',(-0.0242612212587062,0.0370721103911615,0.0851886720151011));
#27543=CARTESIAN_POINT('',(-0.0254986106293532,0.0349288891324553,0.0853209636817677));
#27544=CARTESIAN_POINT('',(-0.0267360000000001,0.0327856678737492,0.0854532553484344));
#27545=CARTESIAN_POINT('',(-0.0267360000000001,0.0303108891324553,0.085585547015101));
#27546=CARTESIAN_POINT('',(-0.0267360000000001,0.0278361103911615,0.0857178386817677));
#27547=CARTESIAN_POINT('',(-0.0254986106293531,0.0256928891324553,0.0858501303484343));
#27548=CARTESIAN_POINT('',(-0.0242612212587062,0.0235496678737492,0.085982422015101));
#27549=CARTESIAN_POINT('',(-0.022118,0.0223122785031023,0.0861147136817677));
#27550=CARTESIAN_POINT('',(-0.0199747787412939,0.0210748891324553,0.0862470053484344));
#27551=CARTESIAN_POINT('',(-0.0175,0.0210748891324553,0.086379297015101));
#27552=CARTESIAN_POINT('',(-0.0150252212587062,0.0210748891324553,0.0865115886817677));
#27553=CARTESIAN_POINT('',(-0.012882,0.0223122785031023,0.0866438803484343));
#27554=CARTESIAN_POINT('',(-0.0107387787412939,0.0235496678737492,0.0867761720151011));
#27555=CARTESIAN_POINT('',(-0.00950138937064695,0.0256928891324553,0.0869084636817677));
#27556=CARTESIAN_POINT('',(-0.00826400000000004,0.0278361103911615,0.0870407553484343));
#27557=CARTESIAN_POINT('',(-0.00826400000000004,0.0303108891324553,0.0871730470151011));
#27558=CARTESIAN_POINT('',(-0.00826400000000004,0.0327856678737492,0.0873053386817677));
#27559=CARTESIAN_POINT('',(-0.00950138937064697,0.0349288891324553,0.0874376303484344));
#27560=CARTESIAN_POINT('',(-0.0107387787412939,0.0370721103911615,0.0875699220151011));
#27561=CARTESIAN_POINT('',(-0.0128820000000001,0.0383094997618084,0.0877022136817677));
#27562=CARTESIAN_POINT('',(-0.0150252212587062,0.0395468891324554,0.0878345053484344));
#27563=CARTESIAN_POINT('',(-0.0175000000000001,0.0395468891324553,0.087966797015101));
#27564=CARTESIAN_POINT('',(-0.0199747787412939,0.0395468891324554,0.0880990886817678));
#27565=CARTESIAN_POINT('',(-0.0221180000000001,0.0383094997618084,0.0882313803484344));
#27566=CARTESIAN_POINT('',(-0.0242612212587062,0.0370721103911615,0.088363672015101));
#27567=CARTESIAN_POINT('',(-0.0254986106293532,0.0349288891324553,0.0884959636817677));
#27568=CARTESIAN_POINT('',(-0.0267360000000001,0.0327856678737492,0.0886282553484344));
#27569=CARTESIAN_POINT('',(-0.0267360000000001,0.0303108891324553,0.088760547015101));
#27570=CARTESIAN_POINT('',(-0.0236094037510318,0.0234951318805056,0.0827365252427255));
#27571=CARTESIAN_POINT('',(-0.0229007397068886,0.0228599104943168,0.0827895910753664));
#27572=CARTESIAN_POINT('',(-0.0220765533185638,0.022384066261155,0.0828409252187621));
#27573=CARTESIAN_POINT('',(-0.0199525675316543,0.0211577824953279,0.0829732168854288));
#27574=CARTESIAN_POINT('',(-0.0175,0.0211577824953279,0.0831055085520954));
#27575=CARTESIAN_POINT('',(-0.0150474324683458,0.0211577824953279,0.0832378002187621));
#27576=CARTESIAN_POINT('',(-0.0129234466814363,0.022384066261155,0.0833700918854287));
#27577=CARTESIAN_POINT('',(-0.0107994608945269,0.0236103500269822,0.0835023835520955));
#27578=CARTESIAN_POINT('',(-0.00957317712869975,0.0257343358138917,0.083634675218762));
#27579=CARTESIAN_POINT('',(-0.00834689336287264,0.0278583216008011,0.0837669668854288));
#27580=CARTESIAN_POINT('',(-0.00834689336287264,0.0303108891324553,0.0838992585520953));
#27581=CARTESIAN_POINT('',(-0.00834689336287265,0.0327634566641096,0.0840315502187621));
#27582=CARTESIAN_POINT('',(-0.00957317712869976,0.034887442451019,0.0841638418854287));
#27583=CARTESIAN_POINT('',(-0.0107994608945269,0.0370114282379285,0.0842961335520954));
#27584=CARTESIAN_POINT('',(-0.0129234466814364,0.0382377120037556,0.084428425218762));
#27585=CARTESIAN_POINT('',(-0.0150474324683458,0.0394639957695827,0.0845607168854288));
#27586=CARTESIAN_POINT('',(-0.0175000000000001,0.0394639957695828,0.0846930085520954));
#27587=CARTESIAN_POINT('',(-0.0199525675316543,0.0394639957695827,0.0848253002187621));
#27588=CARTESIAN_POINT('',(-0.0220765533185638,0.0382377120037556,0.0849575918854288));
#27589=CARTESIAN_POINT('',(-0.0242005391054732,0.0370114282379285,0.0850898835520954));
#27590=CARTESIAN_POINT('',(-0.0254268228713003,0.034887442451019,0.0852221752187621));
#27591=CARTESIAN_POINT('',(-0.0266531066371274,0.0327634566641096,0.0853544668854287));
#27592=CARTESIAN_POINT('',(-0.0266531066371274,0.0303108891324553,0.0854867585520954));
#27593=CARTESIAN_POINT('',(-0.0266531066371274,0.0278583216008011,0.0856190502187621));
#27594=CARTESIAN_POINT('',(-0.0254268228713003,0.0257343358138917,0.0857513418854287));
#27595=CARTESIAN_POINT('',(-0.0242005391054732,0.0236103500269822,0.0858836335520954));
#27596=CARTESIAN_POINT('',(-0.0220765533185638,0.022384066261155,0.0860159252187621));
#27597=CARTESIAN_POINT('',(-0.0199525675316543,0.0211577824953279,0.0861482168854288));
#27598=CARTESIAN_POINT('',(-0.0175,0.0211577824953279,0.0862805085520954));
#27599=CARTESIAN_POINT('',(-0.0150474324683458,0.0211577824953279,0.0864128002187622));
#27600=CARTESIAN_POINT('',(-0.0129234466814363,0.022384066261155,0.0865450918854287));
#27601=CARTESIAN_POINT('',(-0.0107994608945269,0.0236103500269822,0.0866773835520954));
#27602=CARTESIAN_POINT('',(-0.00957317712869975,0.0257343358138917,0.086809675218762));
#27603=CARTESIAN_POINT('',(-0.00834689336287264,0.0278583216008011,0.0869419668854288));
#27604=CARTESIAN_POINT('',(-0.00834689336287264,0.0303108891324553,0.0870742585520954));
#27605=CARTESIAN_POINT('',(-0.00834689336287265,0.0327634566641096,0.0872065502187621));
#27606=CARTESIAN_POINT('',(-0.00957317712869976,0.034887442451019,0.0873388418854287));
#27607=CARTESIAN_POINT('',(-0.0107994608945269,0.0370114282379285,0.0874711335520955));
#27608=CARTESIAN_POINT('',(-0.0129234466814364,0.0382377120037556,0.0876034252187621));
#27609=CARTESIAN_POINT('',(-0.0150474324683458,0.0394639957695827,0.0877357168854287));
#27610=CARTESIAN_POINT('',(-0.0175000000000001,0.0394639957695828,0.0878680085520955));
#27611=CARTESIAN_POINT('',(-0.0199525675316543,0.0394639957695827,0.0880003002187621));
#27612=CARTESIAN_POINT('',(-0.0220765533185638,0.0382377120037556,0.0881325918854288));
#27613=CARTESIAN_POINT('',(-0.0242005391054732,0.0370114282379285,0.0882648835520954));
#27614=CARTESIAN_POINT('',(-0.0254268228713003,0.034887442451019,0.0883971752187621));
#27615=CARTESIAN_POINT('',(-0.0266531066371274,0.0327634566641096,0.0885294668854288));
#27616=CARTESIAN_POINT('',(-0.0266531066371274,0.0303108891324553,0.0886617585520954));
#27617=CARTESIAN_POINT('',(-0.023524635343196,0.0235897009929736,0.0827141317161755));
#27618=CARTESIAN_POINT('',(-0.022825804062635,0.0229632933483092,0.0827671975488165));
#27619=CARTESIAN_POINT('',(-0.0220130533185638,0.0224940514874356,0.0828185316922121));
#27620=CARTESIAN_POINT('',(-0.0199185379842155,0.021284782495328,0.0829508233588788));
#27621=CARTESIAN_POINT('',(-0.0175,0.021284782495328,0.0830831150255454));
#27622=CARTESIAN_POINT('',(-0.0150814620157846,0.021284782495328,0.0832154066922121));
#27623=CARTESIAN_POINT('',(-0.0129869466814363,0.0224940514874357,0.0833476983588788));
#27624=CARTESIAN_POINT('',(-0.0108924313470881,0.0237033204795435,0.0834799900255455));
#27625=CARTESIAN_POINT('',(-0.00968316235498038,0.0257978358138917,0.0836122816922121));
#27626=CARTESIAN_POINT('',(-0.00847389336287265,0.0278923511482399,0.0837445733588788));
#27627=CARTESIAN_POINT('',(-0.00847389336287265,0.0303108891324553,0.0838768650255454));
#27628=CARTESIAN_POINT('',(-0.00847389336287266,0.0327294271166709,0.0840091566922122));
#27629=CARTESIAN_POINT('',(-0.00968316235498039,0.0348239424510191,0.0841414483588788));
#27630=CARTESIAN_POINT('',(-0.0108924313470881,0.0369184577853673,0.0842737400255455));
#27631=CARTESIAN_POINT('',(-0.0129869466814364,0.038127726777475,0.0844060316922121));
#27632=CARTESIAN_POINT('',(-0.0150814620157846,0.0393369957695828,0.0845383233588788));
#27633=CARTESIAN_POINT('',(-0.0175,0.0393369957695828,0.0846706150255454));
#27634=CARTESIAN_POINT('',(-0.0199185379842156,0.0393369957695828,0.0848029066922121));
#27635=CARTESIAN_POINT('',(-0.0220130533185638,0.038127726777475,0.0849351983588788));
#27636=CARTESIAN_POINT('',(-0.024107568652912,0.0369184577853673,0.0850674900255454));
#27637=CARTESIAN_POINT('',(-0.0253168376450197,0.0348239424510191,0.0851997816922121));
#27638=CARTESIAN_POINT('',(-0.0265261066371274,0.0327294271166708,0.0853320733588788));
#27639=CARTESIAN_POINT('',(-0.0265261066371274,0.0303108891324553,0.0854643650255454));
#27640=CARTESIAN_POINT('',(-0.0265261066371274,0.0278923511482398,0.0855966566922121));
#27641=CARTESIAN_POINT('',(-0.0253168376450197,0.0257978358138916,0.0857289483588788));
#27642=CARTESIAN_POINT('',(-0.0241075686529119,0.0237033204795434,0.0858612400255455));
#27643=CARTESIAN_POINT('',(-0.0220130533185638,0.0224940514874356,0.0859935316922121));
#27644=CARTESIAN_POINT('',(-0.0199185379842155,0.021284782495328,0.0861258233588788));
#27645=CARTESIAN_POINT('',(-0.0175,0.021284782495328,0.0862581150255454));
#27646=CARTESIAN_POINT('',(-0.0150814620157846,0.021284782495328,0.0863904066922121));
#27647=CARTESIAN_POINT('',(-0.0129869466814363,0.0224940514874357,0.0865226983588788));
#27648=CARTESIAN_POINT('',(-0.0108924313470881,0.0237033204795435,0.0866549900255455));
#27649=CARTESIAN_POINT('',(-0.00968316235498038,0.0257978358138917,0.0867872816922121));
#27650=CARTESIAN_POINT('',(-0.00847389336287265,0.0278923511482399,0.0869195733588788));
#27651=CARTESIAN_POINT('',(-0.00847389336287265,0.0303108891324553,0.0870518650255454));
#27652=CARTESIAN_POINT('',(-0.00847389336287266,0.0327294271166709,0.0871841566922122));
#27653=CARTESIAN_POINT('',(-0.00968316235498039,0.0348239424510191,0.0873164483588788));
#27654=CARTESIAN_POINT('',(-0.0108924313470881,0.0369184577853673,0.0874487400255455));
#27655=CARTESIAN_POINT('',(-0.0129869466814364,0.038127726777475,0.0875810316922121));
#27656=CARTESIAN_POINT('',(-0.0150814620157846,0.0393369957695828,0.0877133233588788));
#27657=CARTESIAN_POINT('',(-0.0175,0.0393369957695828,0.0878456150255454));
#27658=CARTESIAN_POINT('',(-0.0199185379842156,0.0393369957695828,0.0879779066922121));
#27659=CARTESIAN_POINT('',(-0.0220130533185638,0.038127726777475,0.0881101983588788));
#27660=CARTESIAN_POINT('',(-0.024107568652912,0.0369184577853673,0.0882424900255454));
#27661=CARTESIAN_POINT('',(-0.0253168376450197,0.0348239424510191,0.0883747816922121));
#27662=CARTESIAN_POINT('',(-0.0265261066371274,0.0327294271166708,0.0885070733588787));
#27663=CARTESIAN_POINT('',(-0.0265261066371274,0.0303108891324553,0.0886393650255454));
#27664=CARTESIAN_POINT('',(-0.0231671894155392,0.0230179706406304,0.083));
#27665=CARTESIAN_POINT('',(-0.0226668043442114,0.0226291308389651,0.0830347975716187));
#27666=CARTESIAN_POINT('',(-0.022118,0.0223122785031023,0.0830686728614772));
#27667=CARTESIAN_POINT('',(-0.0199747787412939,0.0210748891324553,0.0832009645281439));
#27668=CARTESIAN_POINT('',(-0.0175,0.0210748891324553,0.0833332561948105));
#27669=CARTESIAN_POINT('',(-0.0150252212587062,0.0210748891324553,0.0834655478614772));
#27670=CARTESIAN_POINT('',(-0.012882,0.0223122785031023,0.0835978395281439));
#27671=CARTESIAN_POINT('',(-0.0107387787412939,0.0235496678737492,0.0837301311948106));
#27672=CARTESIAN_POINT('',(-0.00950138937064696,0.0256928891324554,0.0838624228614772));
#27673=CARTESIAN_POINT('',(-0.00826400000000004,0.0278361103911615,0.0839947145281439));
#27674=CARTESIAN_POINT('',(-0.008264,0.0303108891324553,0.0841270061948105));
#27675=CARTESIAN_POINT('',(-0.00826400000000005,0.0327856678737492,0.0842592978614772));
#27676=CARTESIAN_POINT('',(-0.00950138937064697,0.0349288891324553,0.0843915895281439));
#27677=CARTESIAN_POINT('',(-0.0107387787412939,0.0370721103911615,0.0845238811948106));
#27678=CARTESIAN_POINT('',(-0.012882,0.0383094997618084,0.0846561728614772));
#27679=CARTESIAN_POINT('',(-0.0150252212587062,0.0395468891324554,0.0847884645281439));
#27680=CARTESIAN_POINT('',(-0.0175,0.0395468891324554,0.0849207561948105));
#27681=CARTESIAN_POINT('',(-0.0199747787412939,0.0395468891324554,0.0850530478614772));
#27682=CARTESIAN_POINT('',(-0.022118,0.0383094997618084,0.0851853395281439));
#27683=CARTESIAN_POINT('',(-0.0242612212587062,0.0370721103911615,0.0853176311948106));
#27684=CARTESIAN_POINT('',(-0.0254986106293531,0.0349288891324553,0.0854499228614772));
#27685=CARTESIAN_POINT('',(-0.0267360000000001,0.0327856678737492,0.0855822145281439));
#27686=CARTESIAN_POINT('',(-0.026736,0.0303108891324553,0.0857145061948105));
#27687=CARTESIAN_POINT('',(-0.0267360000000001,0.0278361103911615,0.0858467978614772));
#27688=CARTESIAN_POINT('',(-0.0254986106293531,0.0256928891324554,0.0859790895281439));
#27689=CARTESIAN_POINT('',(-0.0242612212587062,0.0235496678737492,0.0861113811948106));
#27690=CARTESIAN_POINT('',(-0.022118,0.0223122785031023,0.0862436728614772));
#27691=CARTESIAN_POINT('',(-0.0199747787412939,0.0210748891324553,0.0863759645281439));
#27692=CARTESIAN_POINT('',(-0.0175,0.0210748891324553,0.0865082561948105));
#27693=CARTESIAN_POINT('',(-0.0150252212587062,0.0210748891324553,0.0866405478614773));
#27694=CARTESIAN_POINT('',(-0.012882,0.0223122785031023,0.0867728395281439));
#27695=CARTESIAN_POINT('',(-0.0107387787412939,0.0235496678737492,0.0869051311948106));
#27696=CARTESIAN_POINT('',(-0.00950138937064696,0.0256928891324554,0.0870374228614772));
#27697=CARTESIAN_POINT('',(-0.00826400000000004,0.0278361103911615,0.0871697145281439));
#27698=CARTESIAN_POINT('',(-0.008264,0.0303108891324553,0.0873020061948105));
#27699=CARTESIAN_POINT('',(-0.00826400000000005,0.0327856678737492,0.0874342978614772));
#27700=CARTESIAN_POINT('',(-0.00950138937064697,0.0349288891324553,0.0875665895281439));
#27701=CARTESIAN_POINT('',(-0.0107387787412939,0.0370721103911615,0.0876988811948106));
#27702=CARTESIAN_POINT('',(-0.012882,0.0383094997618084,0.0878311728614772));
#27703=CARTESIAN_POINT('',(-0.0150252212587062,0.0395468891324554,0.0879634645281439));
#27704=CARTESIAN_POINT('',(-0.0175,0.0395468891324554,0.0880957561948105));
#27705=CARTESIAN_POINT('',(-0.0199747787412939,0.0395468891324554,0.0882280478614772));
#27706=CARTESIAN_POINT('',(-0.022118,0.0383094997618084,0.0883603395281439));
#27707=CARTESIAN_POINT('',(-0.0242612212587062,0.0370721103911615,0.0884926311948105));
#27708=CARTESIAN_POINT('',(-0.0254986106293531,0.0349288891324553,0.0886249228614772));
#27709=CARTESIAN_POINT('',(-0.0267360000000001,0.0327856678737492,0.0887572145281438));
#27710=CARTESIAN_POINT('',(-0.026736,0.0303108891324553,0.0888895061948105));
#27711=CARTESIAN_POINT('',(-0.0231671894155392,0.0230179706406305,0.083));
#27712=CARTESIAN_POINT('',(-0.026736,0.0303108891324553,0.0888895061948106));
#27713=CARTESIAN_POINT('',(-0.0231671894155392,0.0230179706406305,0.083));
#27714=CARTESIAN_POINT('',(-0.022866367542065,0.0227842076362548,0.083));
#27715=CARTESIAN_POINT('',(-0.022233243984053,0.0223583930718137,0.0830000000000008));
#27716=CARTESIAN_POINT('',(-0.0212143894591252,0.021861314846878,0.0829999999999974));
#27717=CARTESIAN_POINT('',(-0.0203050731606182,0.0215625176281714,0.0830000000000078));
#27718=CARTESIAN_POINT('',(-0.0195554495157663,0.021430163182606,0.0829999999999866));
#27719=CARTESIAN_POINT('',(-0.0191798302521447,0.0213799952297573,0.0830000000000297));
#27720=CARTESIAN_POINT('',(-0.0189864747528848,0.0214080247710879,0.0830000000000297));
#27721=CARTESIAN_POINT('',(-0.026482,0.0303108891324553,0.0888895061948105));
#27722=CARTESIAN_POINT('',(-0.0175,0.0303108891324553,0.0828194520637169));
#27723=CARTESIAN_POINT('',(-0.0265148517458493,0.0283018734529848,0.083));
#27724=CARTESIAN_POINT('',(-0.0262067727498258,0.0269194619051097,0.0830783108961613));
#27725=CARTESIAN_POINT('',(-0.0254986106293531,0.0256928891324554,0.0831540218642768));
#27726=CARTESIAN_POINT('',(-0.0242612212587062,0.0235496678737492,0.0832863135309434));
#27727=CARTESIAN_POINT('',(-0.022118,0.0223122785031023,0.0834186051976101));
#27728=CARTESIAN_POINT('',(-0.0199747787412939,0.0210748891324553,0.0835508968642768));
#27729=CARTESIAN_POINT('',(-0.0175,0.0210748891324553,0.0836831885309434));
#27730=CARTESIAN_POINT('',(-0.0150252212587062,0.0210748891324553,0.0838154801976102));
#27731=CARTESIAN_POINT('',(-0.012882,0.0223122785031023,0.0839477718642768));
#27732=CARTESIAN_POINT('',(-0.0107387787412939,0.0235496678737492,0.0840800635309435));
#27733=CARTESIAN_POINT('',(-0.00950138937064697,0.0256928891324554,0.0842123551976101));
#27734=CARTESIAN_POINT('',(-0.00826400000000004,0.0278361103911615,0.0843446468642768));
#27735=CARTESIAN_POINT('',(-0.008264,0.0303108891324553,0.0844769385309434));
#27736=CARTESIAN_POINT('',(-0.00826400000000005,0.0327856678737492,0.0846092301976101));
#27737=CARTESIAN_POINT('',(-0.00950138937064697,0.0349288891324553,0.0847415218642768));
#27738=CARTESIAN_POINT('',(-0.0107387787412939,0.0370721103911615,0.0848738135309434));
#27739=CARTESIAN_POINT('',(-0.012882,0.0383094997618084,0.0850061051976101));
#27740=CARTESIAN_POINT('',(-0.0150252212587062,0.0395468891324554,0.0851383968642767));
#27741=CARTESIAN_POINT('',(-0.0175,0.0395468891324554,0.0852706885309434));
#27742=CARTESIAN_POINT('',(-0.0199747787412939,0.0395468891324554,0.0854029801976102));
#27743=CARTESIAN_POINT('',(-0.022118,0.0383094997618084,0.0855352718642768));
#27744=CARTESIAN_POINT('',(-0.0242612212587062,0.0370721103911615,0.0856675635309435));
#27745=CARTESIAN_POINT('',(-0.0254986106293531,0.0349288891324553,0.0857998551976101));
#27746=CARTESIAN_POINT('',(-0.0267360000000001,0.0327856678737492,0.0859321468642768));
#27747=CARTESIAN_POINT('',(-0.026736,0.0303108891324553,0.0860644385309434));
#27748=CARTESIAN_POINT('',(-0.0267360000000001,0.0278361103911615,0.0861967301976101));
#27749=CARTESIAN_POINT('',(-0.0254986106293531,0.0256928891324554,0.0863290218642768));
#27750=CARTESIAN_POINT('',(-0.0242612212587062,0.0235496678737492,0.0864613135309434));
#27751=CARTESIAN_POINT('',(-0.022118,0.0223122785031023,0.0865936051976101));
#27752=CARTESIAN_POINT('',(-0.0199747787412939,0.0210748891324553,0.0867258968642769));
#27753=CARTESIAN_POINT('',(-0.0175,0.0210748891324553,0.0868581885309434));
#27754=CARTESIAN_POINT('',(-0.0150252212587062,0.0210748891324553,0.0869904801976102));
#27755=CARTESIAN_POINT('',(-0.012882,0.0223122785031023,0.0871227718642768));
#27756=CARTESIAN_POINT('',(-0.0107387787412939,0.0235496678737492,0.0872550635309435));
#27757=CARTESIAN_POINT('',(-0.00950138937064697,0.0256928891324554,0.0873873551976101));
#27758=CARTESIAN_POINT('',(-0.00826400000000004,0.0278361103911615,0.0875196468642768));
#27759=CARTESIAN_POINT('',(-0.008264,0.0303108891324553,0.0876519385309434));
#27760=CARTESIAN_POINT('',(-0.00826400000000005,0.0327856678737492,0.0877842301976101));
#27761=CARTESIAN_POINT('',(-0.00950138937064697,0.0349288891324553,0.0879165218642768));
#27762=CARTESIAN_POINT('',(-0.0107387787412939,0.0370721103911615,0.0880488135309434));
#27763=CARTESIAN_POINT('',(-0.012882,0.0383094997618084,0.0881811051976101));
#27764=CARTESIAN_POINT('',(-0.0150252212587062,0.0395468891324554,0.0883133968642768));
#27765=CARTESIAN_POINT('',(-0.0175,0.0395468891324554,0.0884456885309434));
#27766=CARTESIAN_POINT('',(-0.0199747787412939,0.0395468891324554,0.0885779801976102));
#27767=CARTESIAN_POINT('',(-0.022118,0.0383094997618084,0.0887102718642768));
#27768=CARTESIAN_POINT('',(-0.0242612212587062,0.0370721103911615,0.0888425635309435));
#27769=CARTESIAN_POINT('',(-0.0254986106293531,0.0349288891324553,0.0889748551976101));
#27770=CARTESIAN_POINT('',(-0.0267360000000001,0.0327856678737492,0.0891071468642768));
#27771=CARTESIAN_POINT('',(-0.026736,0.0303108891324553,0.0892394385309434));
#27772=CARTESIAN_POINT('',(-0.0265148517458494,0.0283018734529848,0.083));
#27773=CARTESIAN_POINT('',(-0.026736,0.0303108891324553,0.0892394385309435));
#27774=CARTESIAN_POINT('',(-0.0175,0.0303108891324553,0.083));
#27775=CARTESIAN_POINT('',(-0.026736,0.0303108891324553,0.089064472362877));
#27776=CARTESIAN_POINT('',(-0.0229058748693024,0.0375225018329433,0.082958966074661));
#27777=CARTESIAN_POINT('',(-0.0243825679779275,0.0364155624426667,0.0830625736532481));
#27778=CARTESIAN_POINT('',(-0.0253053270676696,0.0348172968160874,0.0831636705648742));
#27779=CARTESIAN_POINT('',(-0.0265128153672642,0.0327258657316446,0.083295962231541));
#27780=CARTESIAN_POINT('',(-0.0265128153672642,0.0303108891324553,0.0834282538982076));
#27781=CARTESIAN_POINT('',(-0.0265128153672642,0.0278959125332661,0.0835605455648743));
#27782=CARTESIAN_POINT('',(-0.0253053270676696,0.0258044814488233,0.0836928372315409));
#27783=CARTESIAN_POINT('',(-0.024097838768075,0.0237130503643804,0.0838251288982076));
#27784=CARTESIAN_POINT('',(-0.0220064076836321,0.0225055620647858,0.0839574205648743));
#27785=CARTESIAN_POINT('',(-0.0199149765991893,0.0212980737651912,0.0840897122315409));
#27786=CARTESIAN_POINT('',(-0.0175,0.0212980737651912,0.0842220038982076));
#27787=CARTESIAN_POINT('',(-0.0150850234008108,0.0212980737651912,0.0843542955648742));
#27788=CARTESIAN_POINT('',(-0.012993592316368,0.0225055620647858,0.0844865872315409));
#27789=CARTESIAN_POINT('',(-0.0109021612319251,0.0237130503643804,0.0846188788982076));
#27790=CARTESIAN_POINT('',(-0.00969467293233052,0.0258044814488233,0.0847511705648743));
#27791=CARTESIAN_POINT('',(-0.0084871846327359,0.0278959125332661,0.084883462231541));
#27792=CARTESIAN_POINT('',(-0.0084871846327359,0.0303108891324553,0.0850157538982076));
#27793=CARTESIAN_POINT('',(-0.0084871846327359,0.0327258657316446,0.0851480455648743));
#27794=CARTESIAN_POINT('',(-0.00969467293233052,0.0348172968160874,0.0852803372315409));
#27795=CARTESIAN_POINT('',(-0.0109021612319251,0.0369087279005303,0.0854126288982076));
#27796=CARTESIAN_POINT('',(-0.012993592316368,0.0381162162001248,0.0855449205648742));
#27797=CARTESIAN_POINT('',(-0.0150850234008108,0.0393237044997195,0.0856772122315409));
#27798=CARTESIAN_POINT('',(-0.0175,0.0393237044997195,0.0858095038982076));
#27799=CARTESIAN_POINT('',(-0.0199149765991893,0.0393237044997195,0.0859417955648742));
#27800=CARTESIAN_POINT('',(-0.0220064076836321,0.0381162162001248,0.0860740872315409));
#27801=CARTESIAN_POINT('',(-0.024097838768075,0.0369087279005302,0.0862063788982076));
#27802=CARTESIAN_POINT('',(-0.0253053270676696,0.0348172968160874,0.0863386705648743));
#27803=CARTESIAN_POINT('',(-0.0265128153672642,0.0327258657316446,0.086470962231541));
#27804=CARTESIAN_POINT('',(-0.0265128153672642,0.0303108891324553,0.0866032538982076));
#27805=CARTESIAN_POINT('',(-0.0265128153672642,0.0278959125332661,0.0867355455648743));
#27806=CARTESIAN_POINT('',(-0.0253053270676696,0.0258044814488233,0.0868678372315409));
#27807=CARTESIAN_POINT('',(-0.024097838768075,0.0237130503643804,0.0870001288982076));
#27808=CARTESIAN_POINT('',(-0.0220064076836321,0.0225055620647858,0.0871324205648743));
#27809=CARTESIAN_POINT('',(-0.0199149765991893,0.0212980737651912,0.0872647122315409));
#27810=CARTESIAN_POINT('',(-0.0175,0.0212980737651912,0.0873970038982076));
#27811=CARTESIAN_POINT('',(-0.0150850234008108,0.0212980737651912,0.0875292955648742));
#27812=CARTESIAN_POINT('',(-0.012993592316368,0.0225055620647858,0.0876615872315409));
#27813=CARTESIAN_POINT('',(-0.0109021612319251,0.0237130503643804,0.0877938788982077));
#27814=CARTESIAN_POINT('',(-0.00969467293233052,0.0258044814488233,0.0879261705648742));
#27815=CARTESIAN_POINT('',(-0.0084871846327359,0.0278959125332661,0.088058462231541));
#27816=CARTESIAN_POINT('',(-0.0084871846327359,0.0303108891324553,0.0881907538982076));
#27817=CARTESIAN_POINT('',(-0.0084871846327359,0.0327258657316446,0.0883230455648743));
#27818=CARTESIAN_POINT('',(-0.00969467293233052,0.0348172968160874,0.0884553372315409));
#27819=CARTESIAN_POINT('',(-0.0109021612319251,0.0369087279005303,0.0885876288982076));
#27820=CARTESIAN_POINT('',(-0.012993592316368,0.0381162162001248,0.0887199205648743));
#27821=CARTESIAN_POINT('',(-0.0150850234008108,0.0393237044997195,0.0888522122315409));
#27822=CARTESIAN_POINT('',(-0.0175,0.0393237044997195,0.0889845038982076));
#27823=CARTESIAN_POINT('',(-0.0199149765991893,0.0393237044997195,0.0891167955648742));
#27824=CARTESIAN_POINT('',(-0.0220064076836321,0.0381162162001248,0.0892490872315409));
#27825=CARTESIAN_POINT('',(-0.024097838768075,0.0369087279005302,0.0893813788982077));
#27826=CARTESIAN_POINT('',(-0.0253053270676696,0.0348172968160874,0.0895136705648743));
#27827=CARTESIAN_POINT('',(-0.0265128153672642,0.0327258657316446,0.0896459622315409));
#27828=CARTESIAN_POINT('',(-0.0265128153672642,0.0303108891324553,0.0897782538982076));
#27829=CARTESIAN_POINT('',(-0.0229927332845268,0.0376383737806892,0.0828141534627457));
#27830=CARTESIAN_POINT('',(-0.0244931530287639,0.0365136487398911,0.0829177610413327));
#27831=CARTESIAN_POINT('',(-0.0254307384683766,0.0348897031220451,0.0830188579529589));
#27832=CARTESIAN_POINT('',(-0.0266576279791795,0.0327646681540611,0.0831511496196256));
#27833=CARTESIAN_POINT('',(-0.0266576279791795,0.0303108891324553,0.0832834412862923));
#27834=CARTESIAN_POINT('',(-0.0266576279791795,0.0278571101108495,0.0834157329529589));
#27835=CARTESIAN_POINT('',(-0.0254307384683766,0.0257320751428656,0.0835480246196256));
#27836=CARTESIAN_POINT('',(-0.0242038489575737,0.0236070401748817,0.0836803162862922));
#27837=CARTESIAN_POINT('',(-0.0220788139895898,0.0223801506640788,0.0838126079529589));
#27838=CARTESIAN_POINT('',(-0.0199537790216058,0.0211532611532759,0.0839448996196255));
#27839=CARTESIAN_POINT('',(-0.0175000000000001,0.0211532611532759,0.0840771912862923));
#27840=CARTESIAN_POINT('',(-0.0150462209783943,0.0211532611532759,0.0842094829529589));
#27841=CARTESIAN_POINT('',(-0.0129211860104103,0.0223801506640788,0.0843417746196256));
#27842=CARTESIAN_POINT('',(-0.0107961510424264,0.0236070401748817,0.0844740662862923));
#27843=CARTESIAN_POINT('',(-0.00956926153162349,0.0257320751428656,0.0846063579529589));
#27844=CARTESIAN_POINT('',(-0.00834237202082059,0.0278571101108495,0.0847386496196256));
#27845=CARTESIAN_POINT('',(-0.00834237202082059,0.0303108891324554,0.0848709412862923));
#27846=CARTESIAN_POINT('',(-0.00834237202082059,0.0327646681540611,0.0850032329529589));
#27847=CARTESIAN_POINT('',(-0.00956926153162349,0.0348897031220451,0.0851355246196256));
#27848=CARTESIAN_POINT('',(-0.0107961510424264,0.037014738090029,0.0852678162862922));
#27849=CARTESIAN_POINT('',(-0.0129211860104103,0.0382416276008319,0.085400107952959));
#27850=CARTESIAN_POINT('',(-0.0150462209783943,0.0394685171116348,0.0855323996196256));
#27851=CARTESIAN_POINT('',(-0.0175000000000001,0.0394685171116348,0.0856646912862923));
#27852=CARTESIAN_POINT('',(-0.0199537790216058,0.0394685171116348,0.0857969829529589));
#27853=CARTESIAN_POINT('',(-0.0220788139895898,0.0382416276008319,0.0859292746196256));
#27854=CARTESIAN_POINT('',(-0.0242038489575737,0.037014738090029,0.0860615662862922));
#27855=CARTESIAN_POINT('',(-0.0254307384683766,0.0348897031220451,0.086193857952959));
#27856=CARTESIAN_POINT('',(-0.0266576279791795,0.0327646681540611,0.0863261496196256));
#27857=CARTESIAN_POINT('',(-0.0266576279791795,0.0303108891324553,0.0864584412862923));
#27858=CARTESIAN_POINT('',(-0.0266576279791795,0.0278571101108495,0.0865907329529589));
#27859=CARTESIAN_POINT('',(-0.0254307384683766,0.0257320751428656,0.0867230246196256));
#27860=CARTESIAN_POINT('',(-0.0242038489575737,0.0236070401748817,0.0868553162862923));
#27861=CARTESIAN_POINT('',(-0.0220788139895898,0.0223801506640788,0.086987607952959));
#27862=CARTESIAN_POINT('',(-0.0199537790216058,0.0211532611532759,0.0871198996196256));
#27863=CARTESIAN_POINT('',(-0.0175000000000001,0.0211532611532759,0.0872521912862922));
#27864=CARTESIAN_POINT('',(-0.0150462209783943,0.0211532611532759,0.0873844829529589));
#27865=CARTESIAN_POINT('',(-0.0129211860104103,0.0223801506640788,0.0875167746196255));
#27866=CARTESIAN_POINT('',(-0.0107961510424264,0.0236070401748817,0.0876490662862923));
#27867=CARTESIAN_POINT('',(-0.00956926153162349,0.0257320751428656,0.087781357952959));
#27868=CARTESIAN_POINT('',(-0.00834237202082059,0.0278571101108495,0.0879136496196256));
#27869=CARTESIAN_POINT('',(-0.00834237202082059,0.0303108891324554,0.0880459412862923));
#27870=CARTESIAN_POINT('',(-0.00834237202082059,0.0327646681540611,0.0881782329529589));
#27871=CARTESIAN_POINT('',(-0.00956926153162349,0.0348897031220451,0.0883105246196256));
#27872=CARTESIAN_POINT('',(-0.0107961510424264,0.037014738090029,0.0884428162862923));
#27873=CARTESIAN_POINT('',(-0.0129211860104103,0.0382416276008319,0.0885751079529589));
#27874=CARTESIAN_POINT('',(-0.0150462209783943,0.0394685171116348,0.0887073996196256));
#27875=CARTESIAN_POINT('',(-0.0175000000000001,0.0394685171116348,0.0888396912862922));
#27876=CARTESIAN_POINT('',(-0.0199537790216058,0.0394685171116348,0.0889719829529589));
#27877=CARTESIAN_POINT('',(-0.0220788139895898,0.0382416276008319,0.0891042746196256));
#27878=CARTESIAN_POINT('',(-0.0242038489575737,0.037014738090029,0.0892365662862923));
#27879=CARTESIAN_POINT('',(-0.0254307384683766,0.0348897031220451,0.0893688579529589));
#27880=CARTESIAN_POINT('',(-0.0266576279791795,0.0327646681540611,0.0895011496196256));
#27881=CARTESIAN_POINT('',(-0.0266576279791795,0.0303108891324553,0.0896334412862922));
#27882=CARTESIAN_POINT('',(-0.0230397407201111,0.0377010832269256,0.0826249466671701));
#27883=CARTESIAN_POINT('',(-0.024553001227011,0.0365667326614266,0.0827285542457571));
#27884=CARTESIAN_POINT('',(-0.0254986106293531,0.0349288891324553,0.0828296511573834));
#27885=CARTESIAN_POINT('',(-0.026736,0.0327856678737492,0.08296194282405));
#27886=CARTESIAN_POINT('',(-0.026736,0.0303108891324553,0.0830942344907168));
#27887=CARTESIAN_POINT('',(-0.026736,0.0278361103911615,0.0832265261573834));
#27888=CARTESIAN_POINT('',(-0.0254986106293531,0.0256928891324553,0.08335881782405));
#27889=CARTESIAN_POINT('',(-0.0242612212587062,0.0235496678737492,0.0834911094907167));
#27890=CARTESIAN_POINT('',(-0.022118,0.0223122785031022,0.0836234011573834));
#27891=CARTESIAN_POINT('',(-0.0199747787412939,0.0210748891324553,0.08375569282405));
#27892=CARTESIAN_POINT('',(-0.0175,0.0210748891324553,0.0838879844907167));
#27893=CARTESIAN_POINT('',(-0.0150252212587062,0.0210748891324554,0.0840202761573834));
#27894=CARTESIAN_POINT('',(-0.012882,0.0223122785031022,0.08415256782405));
#27895=CARTESIAN_POINT('',(-0.0107387787412939,0.0235496678737492,0.0842848594907167));
#27896=CARTESIAN_POINT('',(-0.00950138937064696,0.0256928891324553,0.0844171511573834));
#27897=CARTESIAN_POINT('',(-0.00826400000000005,0.0278361103911615,0.08454944282405));
#27898=CARTESIAN_POINT('',(-0.00826400000000005,0.0303108891324554,0.0846817344907167));
#27899=CARTESIAN_POINT('',(-0.00826400000000005,0.0327856678737492,0.0848140261573834));
#27900=CARTESIAN_POINT('',(-0.00950138937064697,0.0349288891324553,0.0849463178240501));
#27901=CARTESIAN_POINT('',(-0.0107387787412939,0.0370721103911615,0.0850786094907167));
#27902=CARTESIAN_POINT('',(-0.0128820000000001,0.0383094997618084,0.0852109011573834));
#27903=CARTESIAN_POINT('',(-0.0150252212587062,0.0395468891324554,0.08534319282405));
#27904=CARTESIAN_POINT('',(-0.0175000000000001,0.0395468891324553,0.0854754844907167));
#27905=CARTESIAN_POINT('',(-0.0199747787412939,0.0395468891324554,0.0856077761573834));
#27906=CARTESIAN_POINT('',(-0.022118,0.0383094997618084,0.0857400678240501));
#27907=CARTESIAN_POINT('',(-0.0242612212587062,0.0370721103911614,0.0858723594907167));
#27908=CARTESIAN_POINT('',(-0.0254986106293531,0.0349288891324553,0.0860046511573834));
#27909=CARTESIAN_POINT('',(-0.026736,0.0327856678737492,0.08613694282405));
#27910=CARTESIAN_POINT('',(-0.026736,0.0303108891324553,0.0862692344907167));
#27911=CARTESIAN_POINT('',(-0.026736,0.0278361103911615,0.0864015261573834));
#27912=CARTESIAN_POINT('',(-0.0254986106293531,0.0256928891324553,0.0865338178240501));
#27913=CARTESIAN_POINT('',(-0.0242612212587062,0.0235496678737492,0.0866661094907167));
#27914=CARTESIAN_POINT('',(-0.022118,0.0223122785031022,0.0867984011573834));
#27915=CARTESIAN_POINT('',(-0.0199747787412939,0.0210748891324553,0.0869306928240501));
#27916=CARTESIAN_POINT('',(-0.0175,0.0210748891324553,0.0870629844907167));
#27917=CARTESIAN_POINT('',(-0.0150252212587062,0.0210748891324554,0.0871952761573834));
#27918=CARTESIAN_POINT('',(-0.012882,0.0223122785031022,0.0873275678240501));
#27919=CARTESIAN_POINT('',(-0.0107387787412939,0.0235496678737492,0.0874598594907167));
#27920=CARTESIAN_POINT('',(-0.00950138937064696,0.0256928891324553,0.0875921511573834));
#27921=CARTESIAN_POINT('',(-0.00826400000000005,0.0278361103911615,0.0877244428240501));
#27922=CARTESIAN_POINT('',(-0.00826400000000005,0.0303108891324554,0.0878567344907168));
#27923=CARTESIAN_POINT('',(-0.00826400000000005,0.0327856678737492,0.0879890261573834));
#27924=CARTESIAN_POINT('',(-0.00950138937064697,0.0349288891324553,0.0881213178240501));
#27925=CARTESIAN_POINT('',(-0.0107387787412939,0.0370721103911615,0.0882536094907168));
#27926=CARTESIAN_POINT('',(-0.0128820000000001,0.0383094997618084,0.0883859011573834));
#27927=CARTESIAN_POINT('',(-0.0150252212587062,0.0395468891324554,0.0885181928240501));
#27928=CARTESIAN_POINT('',(-0.0175000000000001,0.0395468891324553,0.0886504844907168));
#27929=CARTESIAN_POINT('',(-0.0199747787412939,0.0395468891324554,0.0887827761573834));
#27930=CARTESIAN_POINT('',(-0.022118,0.0383094997618084,0.0889150678240501));
#27931=CARTESIAN_POINT('',(-0.0242612212587062,0.0370721103911614,0.0890473594907168));
#27932=CARTESIAN_POINT('',(-0.0254986106293531,0.0349288891324553,0.0891796511573834));
#27933=CARTESIAN_POINT('',(-0.026736,0.0327856678737492,0.0893119428240501));
#27934=CARTESIAN_POINT('',(-0.026736,0.0303108891324553,0.0894442344907167));
#27935=CARTESIAN_POINT('',(-0.0230397407201111,0.0377010832269256,0.0824201507073969));
#27936=CARTESIAN_POINT('',(-0.0245530012270111,0.0365667326614266,0.0825237582859839));
#27937=CARTESIAN_POINT('',(-0.0254986106293531,0.0349288891324553,0.0826248551976101));
#27938=CARTESIAN_POINT('',(-0.0267360000000001,0.0327856678737492,0.0827571468642768));
#27939=CARTESIAN_POINT('',(-0.026736,0.0303108891324553,0.0828894385309434));
#27940=CARTESIAN_POINT('',(-0.0267360000000001,0.0278361103911615,0.0830217301976101));
#27941=CARTESIAN_POINT('',(-0.0254986106293531,0.0256928891324554,0.0831540218642768));
#27942=CARTESIAN_POINT('',(-0.0242612212587062,0.0235496678737492,0.0832863135309434));
#27943=CARTESIAN_POINT('',(-0.022118,0.0223122785031023,0.0834186051976101));
#27944=CARTESIAN_POINT('',(-0.0199747787412939,0.0210748891324553,0.0835508968642768));
#27945=CARTESIAN_POINT('',(-0.0175,0.0210748891324553,0.0836831885309434));
#27946=CARTESIAN_POINT('',(-0.0150252212587062,0.0210748891324554,0.0838154801976102));
#27947=CARTESIAN_POINT('',(-0.012882,0.0223122785031023,0.0839477718642768));
#27948=CARTESIAN_POINT('',(-0.0107387787412939,0.0235496678737492,0.0840800635309435));
#27949=CARTESIAN_POINT('',(-0.00950138937064697,0.0256928891324554,0.0842123551976101));
#27950=CARTESIAN_POINT('',(-0.00826400000000004,0.0278361103911615,0.0843446468642768));
#27951=CARTESIAN_POINT('',(-0.008264,0.0303108891324553,0.0844769385309434));
#27952=CARTESIAN_POINT('',(-0.00826400000000005,0.0327856678737492,0.0846092301976101));
#27953=CARTESIAN_POINT('',(-0.00950138937064697,0.0349288891324553,0.0847415218642768));
#27954=CARTESIAN_POINT('',(-0.0107387787412939,0.0370721103911615,0.0848738135309434));
#27955=CARTESIAN_POINT('',(-0.012882,0.0383094997618084,0.0850061051976101));
#27956=CARTESIAN_POINT('',(-0.0150252212587062,0.0395468891324554,0.0851383968642767));
#27957=CARTESIAN_POINT('',(-0.0175,0.0395468891324554,0.0852706885309434));
#27958=CARTESIAN_POINT('',(-0.0199747787412939,0.0395468891324554,0.0854029801976102));
#27959=CARTESIAN_POINT('',(-0.022118,0.0383094997618084,0.0855352718642768));
#27960=CARTESIAN_POINT('',(-0.0242612212587062,0.0370721103911615,0.0856675635309435));
#27961=CARTESIAN_POINT('',(-0.0254986106293531,0.0349288891324553,0.0857998551976101));
#27962=CARTESIAN_POINT('',(-0.0267360000000001,0.0327856678737492,0.0859321468642768));
#27963=CARTESIAN_POINT('',(-0.026736,0.0303108891324553,0.0860644385309434));
#27964=CARTESIAN_POINT('',(-0.0267360000000001,0.0278361103911615,0.0861967301976101));
#27965=CARTESIAN_POINT('',(-0.0254986106293531,0.0256928891324554,0.0863290218642768));
#27966=CARTESIAN_POINT('',(-0.0242612212587062,0.0235496678737492,0.0864613135309434));
#27967=CARTESIAN_POINT('',(-0.022118,0.0223122785031023,0.0865936051976101));
#27968=CARTESIAN_POINT('',(-0.0199747787412939,0.0210748891324553,0.0867258968642769));
#27969=CARTESIAN_POINT('',(-0.0175,0.0210748891324553,0.0868581885309434));
#27970=CARTESIAN_POINT('',(-0.0150252212587062,0.0210748891324554,0.0869904801976102));
#27971=CARTESIAN_POINT('',(-0.012882,0.0223122785031023,0.0871227718642768));
#27972=CARTESIAN_POINT('',(-0.0107387787412939,0.0235496678737492,0.0872550635309435));
#27973=CARTESIAN_POINT('',(-0.00950138937064697,0.0256928891324554,0.0873873551976101));
#27974=CARTESIAN_POINT('',(-0.00826400000000004,0.0278361103911615,0.0875196468642768));
#27975=CARTESIAN_POINT('',(-0.008264,0.0303108891324553,0.0876519385309434));
#27976=CARTESIAN_POINT('',(-0.00826400000000005,0.0327856678737492,0.0877842301976101));
#27977=CARTESIAN_POINT('',(-0.00950138937064697,0.0349288891324553,0.0879165218642768));
#27978=CARTESIAN_POINT('',(-0.0107387787412939,0.0370721103911615,0.0880488135309434));
#27979=CARTESIAN_POINT('',(-0.012882,0.0383094997618084,0.0881811051976101));
#27980=CARTESIAN_POINT('',(-0.0150252212587062,0.0395468891324554,0.0883133968642768));
#27981=CARTESIAN_POINT('',(-0.0175,0.0395468891324554,0.0884456885309434));
#27982=CARTESIAN_POINT('',(-0.0199747787412939,0.0395468891324554,0.0885779801976102));
#27983=CARTESIAN_POINT('',(-0.022118,0.0383094997618084,0.0887102718642768));
#27984=CARTESIAN_POINT('',(-0.0242612212587062,0.0370721103911615,0.0888425635309435));
#27985=CARTESIAN_POINT('',(-0.0254986106293531,0.0349288891324553,0.0889748551976101));
#27986=CARTESIAN_POINT('',(-0.0267360000000001,0.0327856678737492,0.0891071468642768));
#27987=CARTESIAN_POINT('',(-0.026736,0.0303108891324553,0.0892394385309434));
#27988=CARTESIAN_POINT('',(-0.0234697589126183,0.0370631346381821,0.0830000000000001));
#27989=CARTESIAN_POINT('',(-0.0245706194344714,0.0360898477654954,0.0830831764537999));
#27990=CARTESIAN_POINT('',(-0.0253053270676696,0.0348172968160874,0.0831636705648742));
#27991=CARTESIAN_POINT('',(-0.0265128153672642,0.0327258657316446,0.083295962231541));
#27992=CARTESIAN_POINT('',(-0.0265128153672642,0.0303108891324553,0.0834282538982076));
#27993=CARTESIAN_POINT('',(-0.0265128153672642,0.0278959125332661,0.0835605455648743));
#27994=CARTESIAN_POINT('',(-0.0253053270676696,0.0258044814488233,0.0836928372315409));
#27995=CARTESIAN_POINT('',(-0.024097838768075,0.0237130503643804,0.0838251288982076));
#27996=CARTESIAN_POINT('',(-0.0220064076836321,0.0225055620647858,0.0839574205648743));
#27997=CARTESIAN_POINT('',(-0.0199149765991893,0.0212980737651912,0.0840897122315409));
#27998=CARTESIAN_POINT('',(-0.0175,0.0212980737651912,0.0842220038982076));
#27999=CARTESIAN_POINT('',(-0.0150850234008108,0.0212980737651912,0.0843542955648742));
#28000=CARTESIAN_POINT('',(-0.012993592316368,0.0225055620647858,0.0844865872315409));
#28001=CARTESIAN_POINT('',(-0.0109021612319251,0.0237130503643804,0.0846188788982076));
#28002=CARTESIAN_POINT('',(-0.00969467293233052,0.0258044814488233,0.0847511705648743));
#28003=CARTESIAN_POINT('',(-0.00848718463273591,0.0278959125332661,0.084883462231541));
#28004=CARTESIAN_POINT('',(-0.0084871846327359,0.0303108891324553,0.0850157538982076));
#28005=CARTESIAN_POINT('',(-0.00848718463273591,0.0327258657316446,0.0851480455648743));
#28006=CARTESIAN_POINT('',(-0.00969467293233052,0.0348172968160874,0.0852803372315409));
#28007=CARTESIAN_POINT('',(-0.0109021612319251,0.0369087279005303,0.0854126288982076));
#28008=CARTESIAN_POINT('',(-0.012993592316368,0.0381162162001248,0.0855449205648742));
#28009=CARTESIAN_POINT('',(-0.0150850234008108,0.0393237044997195,0.0856772122315409));
#28010=CARTESIAN_POINT('',(-0.0175,0.0393237044997195,0.0858095038982076));
#28011=CARTESIAN_POINT('',(-0.0199149765991893,0.0393237044997195,0.0859417955648742));
#28012=CARTESIAN_POINT('',(-0.0220064076836321,0.0381162162001248,0.0860740872315409));
#28013=CARTESIAN_POINT('',(-0.024097838768075,0.0369087279005302,0.0862063788982076));
#28014=CARTESIAN_POINT('',(-0.0253053270676696,0.0348172968160874,0.0863386705648743));
#28015=CARTESIAN_POINT('',(-0.0265128153672642,0.0327258657316446,0.086470962231541));
#28016=CARTESIAN_POINT('',(-0.0265128153672642,0.0303108891324553,0.0866032538982076));
#28017=CARTESIAN_POINT('',(-0.0265128153672642,0.0278959125332661,0.0867355455648743));
#28018=CARTESIAN_POINT('',(-0.0253053270676696,0.0258044814488233,0.0868678372315409));
#28019=CARTESIAN_POINT('',(-0.024097838768075,0.0237130503643804,0.0870001288982076));
#28020=CARTESIAN_POINT('',(-0.0220064076836321,0.0225055620647858,0.0871324205648743));
#28021=CARTESIAN_POINT('',(-0.0199149765991893,0.0212980737651912,0.0872647122315409));
#28022=CARTESIAN_POINT('',(-0.0175,0.0212980737651912,0.0873970038982076));
#28023=CARTESIAN_POINT('',(-0.0150850234008108,0.0212980737651912,0.0875292955648742));
#28024=CARTESIAN_POINT('',(-0.012993592316368,0.0225055620647858,0.0876615872315409));
#28025=CARTESIAN_POINT('',(-0.0109021612319251,0.0237130503643804,0.0877938788982077));
#28026=CARTESIAN_POINT('',(-0.00969467293233052,0.0258044814488233,0.0879261705648742));
#28027=CARTESIAN_POINT('',(-0.00848718463273591,0.0278959125332661,0.088058462231541));
#28028=CARTESIAN_POINT('',(-0.0084871846327359,0.0303108891324553,0.0881907538982076));
#28029=CARTESIAN_POINT('',(-0.00848718463273591,0.0327258657316446,0.0883230455648743));
#28030=CARTESIAN_POINT('',(-0.00969467293233052,0.0348172968160874,0.0884553372315409));
#28031=CARTESIAN_POINT('',(-0.0109021612319251,0.0369087279005303,0.0885876288982076));
#28032=CARTESIAN_POINT('',(-0.012993592316368,0.0381162162001248,0.0887199205648743));
#28033=CARTESIAN_POINT('',(-0.0150850234008108,0.0393237044997195,0.0888522122315409));
#28034=CARTESIAN_POINT('',(-0.0175,0.0393237044997195,0.0889845038982076));
#28035=CARTESIAN_POINT('',(-0.0199149765991893,0.0393237044997195,0.0891167955648742));
#28036=CARTESIAN_POINT('',(-0.0220064076836321,0.0381162162001248,0.0892490872315409));
#28037=CARTESIAN_POINT('',(-0.024097838768075,0.0369087279005302,0.0893813788982077));
#28038=CARTESIAN_POINT('',(-0.0253053270676696,0.0348172968160874,0.0895136705648743));
#28039=CARTESIAN_POINT('',(-0.0265128153672642,0.0327258657316446,0.0896459622315409));
#28040=CARTESIAN_POINT('',(-0.0265128153672642,0.0303108891324553,0.0897782538982076));
#28041=CARTESIAN_POINT('',(-0.0234697589126183,0.0370631346381822,0.083));
#28042=CARTESIAN_POINT('',(-0.0265128153672642,0.0303108891324553,0.0897782538982076));
#28043=CARTESIAN_POINT('',(-0.0234697589126183,0.0370631346381822,0.083));
#28044=CARTESIAN_POINT('',(-0.02476030267836,0.0360460956012747,0.083));
#28045=CARTESIAN_POINT('',(-0.0262028298061085,0.0339579466917452,0.0829999999999999));
#28046=CARTESIAN_POINT('',(-0.0268263894154986,0.0307216863639011,0.083));
#28047=CARTESIAN_POINT('',(-0.0266934574485126,0.0291033126587244,0.083));
#28048=CARTESIAN_POINT('',(-0.0265148517458493,0.0283018734529848,0.083));
#28049=CARTESIAN_POINT('',(-0.025974,0.0303108891324553,0.0892394385309434));
#28050=CARTESIAN_POINT('',(-0.0128220863881535,0.037278617891806,0.0829566731169614));
#28051=CARTESIAN_POINT('',(-0.0130578663098391,0.0374369131043705,0.0829736444091975));
#28052=CARTESIAN_POINT('',(-0.0133038076836321,0.0375789074227348,0.0829903512994025));
#28053=CARTESIAN_POINT('',(-0.0152512673150871,0.0387032737651912,0.0831226429660692));
#28054=CARTESIAN_POINT('',(-0.0175,0.0387032737651912,0.0832549346327359));
#28055=CARTESIAN_POINT('',(-0.019748732684913,0.0387032737651912,0.0833872262994025));
#28056=CARTESIAN_POINT('',(-0.021696192316368,0.0375789074227348,0.0835195179660692));
#28057=CARTESIAN_POINT('',(-0.023643651947823,0.0364545410802783,0.083651809632736));
#28058=CARTESIAN_POINT('',(-0.0247680182902794,0.0345070814488233,0.0837841012994025));
#28059=CARTESIAN_POINT('',(-0.0258923846327359,0.0325596218173683,0.0839163929660693));
#28060=CARTESIAN_POINT('',(-0.0258923846327359,0.0303108891324553,0.0840486846327359));
#28061=CARTESIAN_POINT('',(-0.0258923846327359,0.0280621564475424,0.0841809762994026));
#28062=CARTESIAN_POINT('',(-0.0247680182902794,0.0261146968160874,0.0843132679660692));
#28063=CARTESIAN_POINT('',(-0.023643651947823,0.0241672371846324,0.0844455596327359));
#28064=CARTESIAN_POINT('',(-0.021696192316368,0.023042870842176,0.0845778512994025));
#28065=CARTESIAN_POINT('',(-0.019748732684913,0.0219185044997195,0.0847101429660692));
#28066=CARTESIAN_POINT('',(-0.0175,0.0219185044997195,0.0848424346327359));
#28067=CARTESIAN_POINT('',(-0.0152512673150871,0.0219185044997195,0.0849747262994025));
#28068=CARTESIAN_POINT('',(-0.0133038076836321,0.023042870842176,0.0851070179660692));
#28069=CARTESIAN_POINT('',(-0.0113563480521771,0.0241672371846324,0.0852393096327359));
#28070=CARTESIAN_POINT('',(-0.0102319817097207,0.0261146968160874,0.0853716012994025));
#28071=CARTESIAN_POINT('',(-0.00910761536726418,0.0280621564475424,0.0855038929660693));
#28072=CARTESIAN_POINT('',(-0.00910761536726419,0.0303108891324553,0.0856361846327359));
#28073=CARTESIAN_POINT('',(-0.00910761536726419,0.0325596218173683,0.0857684762994026));
#28074=CARTESIAN_POINT('',(-0.0102319817097207,0.0345070814488233,0.0859007679660692));
#28075=CARTESIAN_POINT('',(-0.0113563480521771,0.0364545410802783,0.0860330596327359));
#28076=CARTESIAN_POINT('',(-0.0133038076836321,0.0375789074227348,0.0861653512994025));
#28077=CARTESIAN_POINT('',(-0.0152512673150871,0.0387032737651912,0.0862976429660692));
#28078=CARTESIAN_POINT('',(-0.0175,0.0387032737651912,0.0864299346327359));
#28079=CARTESIAN_POINT('',(-0.019748732684913,0.0387032737651912,0.0865622262994026));
#28080=CARTESIAN_POINT('',(-0.021696192316368,0.0375789074227348,0.0866945179660692));
#28081=CARTESIAN_POINT('',(-0.023643651947823,0.0364545410802783,0.0868268096327359));
#28082=CARTESIAN_POINT('',(-0.0247680182902794,0.0345070814488233,0.0869591012994025));
#28083=CARTESIAN_POINT('',(-0.0258923846327359,0.0325596218173683,0.0870913929660692));
#28084=CARTESIAN_POINT('',(-0.0258923846327359,0.0303108891324553,0.0872236846327359));
#28085=CARTESIAN_POINT('',(-0.0258923846327359,0.0280621564475424,0.0873559762994026));
#28086=CARTESIAN_POINT('',(-0.0247680182902794,0.0261146968160874,0.0874882679660692));
#28087=CARTESIAN_POINT('',(-0.023643651947823,0.0241672371846324,0.0876205596327359));
#28088=CARTESIAN_POINT('',(-0.021696192316368,0.023042870842176,0.0877528512994025));
#28089=CARTESIAN_POINT('',(-0.019748732684913,0.0219185044997195,0.0878851429660692));
#28090=CARTESIAN_POINT('',(-0.0175,0.0219185044997195,0.0880174346327359));
#28091=CARTESIAN_POINT('',(-0.0152512673150871,0.0219185044997195,0.0881497262994026));
#28092=CARTESIAN_POINT('',(-0.0133038076836321,0.023042870842176,0.0882820179660692));
#28093=CARTESIAN_POINT('',(-0.0113563480521771,0.0241672371846324,0.0884143096327359));
#28094=CARTESIAN_POINT('',(-0.0102319817097207,0.0261146968160874,0.0885466012994025));
#28095=CARTESIAN_POINT('',(-0.00910761536726418,0.0280621564475424,0.0886788929660693));
#28096=CARTESIAN_POINT('',(-0.00910761536726419,0.0303108891324553,0.0888111846327359));
#28097=CARTESIAN_POINT('',(-0.00910761536726419,0.0325596218173683,0.0889434762994026));
#28098=CARTESIAN_POINT('',(-0.0102319817097207,0.0345070814488233,0.0890757679660692));
#28099=CARTESIAN_POINT('',(-0.0113563480521771,0.0364545410802783,0.0892080596327359));
#28100=CARTESIAN_POINT('',(-0.0133038076836321,0.0375789074227348,0.0893403512994025));
#28101=CARTESIAN_POINT('',(-0.0152512673150871,0.0387032737651912,0.0894726429660692));
#28102=CARTESIAN_POINT('',(-0.0175,0.0387032737651912,0.0896049346327359));
#28103=CARTESIAN_POINT('',(-0.019748732684913,0.0387032737651912,0.0897372262994026));
#28104=CARTESIAN_POINT('',(-0.021696192316368,0.0375789074227348,0.0898695179660692));
#28105=CARTESIAN_POINT('',(-0.023643651947823,0.0364545410802783,0.0900018096327359));
#28106=CARTESIAN_POINT('',(-0.0247680182902794,0.0345070814488233,0.0901341012994025));
#28107=CARTESIAN_POINT('',(-0.0258923846327359,0.0325596218173683,0.0902663929660692));
#28108=CARTESIAN_POINT('',(-0.0258923846327359,0.0303108891324553,0.0903986846327359));
#28109=CARTESIAN_POINT('',(-0.0124762584137138,0.0377937269175881,0.0823362423824331));
#28110=CARTESIAN_POINT('',(-0.0127294690319654,0.0379637245507758,0.0823532136746692));
#28111=CARTESIAN_POINT('',(-0.012993592316368,0.0381162162001248,0.0823699205648742));
#28112=CARTESIAN_POINT('',(-0.0150850234008108,0.0393237044997195,0.0825022122315409));
#28113=CARTESIAN_POINT('',(-0.0175,0.0393237044997195,0.0826345038982076));
#28114=CARTESIAN_POINT('',(-0.0199149765991893,0.0393237044997195,0.0827667955648743));
#28115=CARTESIAN_POINT('',(-0.0220064076836321,0.0381162162001248,0.0828990872315409));
#28116=CARTESIAN_POINT('',(-0.024097838768075,0.0369087279005302,0.0830313788982076));
#28117=CARTESIAN_POINT('',(-0.0253053270676696,0.0348172968160874,0.0831636705648742));
#28118=CARTESIAN_POINT('',(-0.0265128153672642,0.0327258657316446,0.083295962231541));
#28119=CARTESIAN_POINT('',(-0.0265128153672642,0.0303108891324553,0.0834282538982076));
#28120=CARTESIAN_POINT('',(-0.0265128153672642,0.0278959125332661,0.0835605455648743));
#28121=CARTESIAN_POINT('',(-0.0253053270676696,0.0258044814488233,0.0836928372315409));
#28122=CARTESIAN_POINT('',(-0.024097838768075,0.0237130503643804,0.0838251288982076));
#28123=CARTESIAN_POINT('',(-0.0220064076836321,0.0225055620647858,0.0839574205648743));
#28124=CARTESIAN_POINT('',(-0.0199149765991893,0.0212980737651912,0.0840897122315409));
#28125=CARTESIAN_POINT('',(-0.0175,0.0212980737651912,0.0842220038982076));
#28126=CARTESIAN_POINT('',(-0.0150850234008108,0.0212980737651912,0.0843542955648742));
#28127=CARTESIAN_POINT('',(-0.012993592316368,0.0225055620647858,0.0844865872315409));
#28128=CARTESIAN_POINT('',(-0.0109021612319251,0.0237130503643804,0.0846188788982076));
#28129=CARTESIAN_POINT('',(-0.00969467293233052,0.0258044814488233,0.0847511705648743));
#28130=CARTESIAN_POINT('',(-0.0084871846327359,0.0278959125332661,0.084883462231541));
#28131=CARTESIAN_POINT('',(-0.0084871846327359,0.0303108891324553,0.0850157538982076));
#28132=CARTESIAN_POINT('',(-0.0084871846327359,0.0327258657316446,0.0851480455648743));
#28133=CARTESIAN_POINT('',(-0.00969467293233052,0.0348172968160874,0.0852803372315409));
#28134=CARTESIAN_POINT('',(-0.0109021612319251,0.0369087279005303,0.0854126288982076));
#28135=CARTESIAN_POINT('',(-0.012993592316368,0.0381162162001248,0.0855449205648742));
#28136=CARTESIAN_POINT('',(-0.0150850234008108,0.0393237044997195,0.0856772122315409));
#28137=CARTESIAN_POINT('',(-0.0175,0.0393237044997195,0.0858095038982076));
#28138=CARTESIAN_POINT('',(-0.0199149765991893,0.0393237044997195,0.0859417955648742));
#28139=CARTESIAN_POINT('',(-0.0220064076836321,0.0381162162001248,0.0860740872315409));
#28140=CARTESIAN_POINT('',(-0.024097838768075,0.0369087279005302,0.0862063788982076));
#28141=CARTESIAN_POINT('',(-0.0253053270676696,0.0348172968160874,0.0863386705648743));
#28142=CARTESIAN_POINT('',(-0.0265128153672642,0.0327258657316446,0.086470962231541));
#28143=CARTESIAN_POINT('',(-0.0265128153672642,0.0303108891324553,0.0866032538982076));
#28144=CARTESIAN_POINT('',(-0.0265128153672642,0.0278959125332661,0.0867355455648743));
#28145=CARTESIAN_POINT('',(-0.0253053270676696,0.0258044814488233,0.0868678372315409));
#28146=CARTESIAN_POINT('',(-0.024097838768075,0.0237130503643804,0.0870001288982076));
#28147=CARTESIAN_POINT('',(-0.0220064076836321,0.0225055620647858,0.0871324205648743));
#28148=CARTESIAN_POINT('',(-0.0199149765991893,0.0212980737651912,0.0872647122315409));
#28149=CARTESIAN_POINT('',(-0.0175,0.0212980737651912,0.0873970038982076));
#28150=CARTESIAN_POINT('',(-0.0150850234008108,0.0212980737651912,0.0875292955648742));
#28151=CARTESIAN_POINT('',(-0.012993592316368,0.0225055620647858,0.0876615872315409));
#28152=CARTESIAN_POINT('',(-0.0109021612319251,0.0237130503643804,0.0877938788982077));
#28153=CARTESIAN_POINT('',(-0.00969467293233052,0.0258044814488233,0.0879261705648742));
#28154=CARTESIAN_POINT('',(-0.0084871846327359,0.0278959125332661,0.088058462231541));
#28155=CARTESIAN_POINT('',(-0.0084871846327359,0.0303108891324553,0.0881907538982076));
#28156=CARTESIAN_POINT('',(-0.0084871846327359,0.0327258657316446,0.0883230455648743));
#28157=CARTESIAN_POINT('',(-0.00969467293233052,0.0348172968160874,0.0884553372315409));
#28158=CARTESIAN_POINT('',(-0.0109021612319251,0.0369087279005303,0.0885876288982076));
#28159=CARTESIAN_POINT('',(-0.012993592316368,0.0381162162001248,0.0887199205648743));
#28160=CARTESIAN_POINT('',(-0.0150850234008108,0.0393237044997195,0.0888522122315409));
#28161=CARTESIAN_POINT('',(-0.0175,0.0393237044997195,0.0889845038982076));
#28162=CARTESIAN_POINT('',(-0.0199149765991893,0.0393237044997195,0.0891167955648742));
#28163=CARTESIAN_POINT('',(-0.0220064076836321,0.0381162162001248,0.0892490872315409));
#28164=CARTESIAN_POINT('',(-0.024097838768075,0.0369087279005302,0.0893813788982077));
#28165=CARTESIAN_POINT('',(-0.0253053270676696,0.0348172968160874,0.0895136705648743));
#28166=CARTESIAN_POINT('',(-0.0265128153672642,0.0327258657316446,0.0896459622315409));
#28167=CARTESIAN_POINT('',(-0.0265128153672642,0.0303108891324553,0.0897782538982076));
#28168=CARTESIAN_POINT('',(-0.0134462729974218,0.0376593187070208,0.0830000000000001));
#28169=CARTESIAN_POINT('',(-0.0153387117874777,0.0387032737651912,0.0831277872747151));
#28170=CARTESIAN_POINT('',(-0.0175,0.0387032737651912,0.0832549346327359));
#28171=CARTESIAN_POINT('',(-0.019748732684913,0.0387032737651912,0.0833872262994025));
#28172=CARTESIAN_POINT('',(-0.021696192316368,0.0375789074227348,0.0835195179660692));
#28173=CARTESIAN_POINT('',(-0.023643651947823,0.0364545410802783,0.083651809632736));
#28174=CARTESIAN_POINT('',(-0.0247680182902794,0.0345070814488233,0.0837841012994025));
#28175=CARTESIAN_POINT('',(-0.0258923846327359,0.0325596218173683,0.0839163929660692));
#28176=CARTESIAN_POINT('',(-0.0258923846327359,0.0303108891324553,0.0840486846327359));
#28177=CARTESIAN_POINT('',(-0.0258923846327359,0.0280621564475424,0.0841809762994026));
#28178=CARTESIAN_POINT('',(-0.0247680182902794,0.0261146968160874,0.0843132679660692));
#28179=CARTESIAN_POINT('',(-0.023643651947823,0.0241672371846324,0.0844455596327359));
#28180=CARTESIAN_POINT('',(-0.021696192316368,0.023042870842176,0.0845778512994025));
#28181=CARTESIAN_POINT('',(-0.019748732684913,0.0219185044997195,0.0847101429660692));
#28182=CARTESIAN_POINT('',(-0.0175,0.0219185044997195,0.0848424346327359));
#28183=CARTESIAN_POINT('',(-0.0152512673150871,0.0219185044997195,0.0849747262994025));
#28184=CARTESIAN_POINT('',(-0.0133038076836321,0.023042870842176,0.0851070179660692));
#28185=CARTESIAN_POINT('',(-0.0113563480521771,0.0241672371846324,0.0852393096327359));
#28186=CARTESIAN_POINT('',(-0.0102319817097207,0.0261146968160874,0.0853716012994025));
#28187=CARTESIAN_POINT('',(-0.00910761536726419,0.0280621564475424,0.0855038929660693));
#28188=CARTESIAN_POINT('',(-0.00910761536726419,0.0303108891324553,0.0856361846327359));
#28189=CARTESIAN_POINT('',(-0.00910761536726419,0.0325596218173683,0.0857684762994026));
#28190=CARTESIAN_POINT('',(-0.0102319817097207,0.0345070814488233,0.0859007679660692));
#28191=CARTESIAN_POINT('',(-0.0113563480521771,0.0364545410802783,0.0860330596327359));
#28192=CARTESIAN_POINT('',(-0.0133038076836321,0.0375789074227348,0.0861653512994025));
#28193=CARTESIAN_POINT('',(-0.0152512673150871,0.0387032737651912,0.0862976429660692));
#28194=CARTESIAN_POINT('',(-0.0175,0.0387032737651912,0.0864299346327359));
#28195=CARTESIAN_POINT('',(-0.019748732684913,0.0387032737651912,0.0865622262994026));
#28196=CARTESIAN_POINT('',(-0.021696192316368,0.0375789074227348,0.0866945179660692));
#28197=CARTESIAN_POINT('',(-0.023643651947823,0.0364545410802783,0.0868268096327359));
#28198=CARTESIAN_POINT('',(-0.0247680182902794,0.0345070814488233,0.0869591012994025));
#28199=CARTESIAN_POINT('',(-0.0258923846327359,0.0325596218173683,0.0870913929660692));
#28200=CARTESIAN_POINT('',(-0.0258923846327359,0.0303108891324553,0.0872236846327359));
#28201=CARTESIAN_POINT('',(-0.0258923846327359,0.0280621564475424,0.0873559762994026));
#28202=CARTESIAN_POINT('',(-0.0247680182902794,0.0261146968160874,0.0874882679660692));
#28203=CARTESIAN_POINT('',(-0.023643651947823,0.0241672371846324,0.0876205596327359));
#28204=CARTESIAN_POINT('',(-0.021696192316368,0.023042870842176,0.0877528512994025));
#28205=CARTESIAN_POINT('',(-0.019748732684913,0.0219185044997195,0.0878851429660692));
#28206=CARTESIAN_POINT('',(-0.0175,0.0219185044997195,0.0880174346327359));
#28207=CARTESIAN_POINT('',(-0.0152512673150871,0.0219185044997195,0.0881497262994026));
#28208=CARTESIAN_POINT('',(-0.0133038076836321,0.023042870842176,0.0882820179660692));
#28209=CARTESIAN_POINT('',(-0.0113563480521771,0.0241672371846324,0.0884143096327359));
#28210=CARTESIAN_POINT('',(-0.0102319817097207,0.0261146968160874,0.0885466012994025));
#28211=CARTESIAN_POINT('',(-0.00910761536726419,0.0280621564475424,0.0886788929660692));
#28212=CARTESIAN_POINT('',(-0.00910761536726419,0.0303108891324553,0.0888111846327359));
#28213=CARTESIAN_POINT('',(-0.00910761536726419,0.0325596218173683,0.0889434762994026));
#28214=CARTESIAN_POINT('',(-0.0102319817097207,0.0345070814488233,0.0890757679660692));
#28215=CARTESIAN_POINT('',(-0.0113563480521771,0.0364545410802783,0.0892080596327359));
#28216=CARTESIAN_POINT('',(-0.0133038076836321,0.0375789074227348,0.0893403512994025));
#28217=CARTESIAN_POINT('',(-0.0152512673150871,0.0387032737651912,0.0894726429660692));
#28218=CARTESIAN_POINT('',(-0.0175,0.0387032737651912,0.0896049346327359));
#28219=CARTESIAN_POINT('',(-0.019748732684913,0.0387032737651912,0.0897372262994026));
#28220=CARTESIAN_POINT('',(-0.021696192316368,0.0375789074227348,0.0898695179660692));
#28221=CARTESIAN_POINT('',(-0.023643651947823,0.0364545410802783,0.0900018096327359));
#28222=CARTESIAN_POINT('',(-0.0247680182902794,0.0345070814488233,0.0901341012994025));
#28223=CARTESIAN_POINT('',(-0.0258923846327359,0.0325596218173683,0.0902663929660692));
#28224=CARTESIAN_POINT('',(-0.0258923846327359,0.0303108891324553,0.0903986846327359));
#28225=CARTESIAN_POINT('',(-0.0134462729974218,0.0376593187070208,0.083));
#28226=CARTESIAN_POINT('',(-0.0258923846327359,0.0303108891324553,0.0903986846327359));
#28227=CARTESIAN_POINT('',(-0.0134462729974218,0.0376593187070208,0.083));
#28228=CARTESIAN_POINT('',(-0.0149685242548422,0.038620412767118,0.083));
#28229=CARTESIAN_POINT('',(-0.0176826196805459,0.0392910823435752,0.083));
#28230=CARTESIAN_POINT('',(-0.0212176395987549,0.0385051138778108,0.0830000000000001));
#28231=CARTESIAN_POINT('',(-0.0227632438890936,0.0376199180485249,0.083));
#28232=CARTESIAN_POINT('',(-0.0234697589126183,0.0370631346381822,0.083));
#28233=CARTESIAN_POINT('',(-0.0262026,0.0303108891324553,0.0900884692654717));
#28234=CARTESIAN_POINT('',(-0.0093308,0.0303108891324553,0.083));
#28235=CARTESIAN_POINT('',(-0.00933080000000005,0.0324998196752637,0.0831322916666668));
#28236=CARTESIAN_POINT('',(-0.0104252652714042,0.0343954891324554,0.0832645833333334));
#28237=CARTESIAN_POINT('',(-0.0115197305428084,0.036291158589647,0.0833968750000001));
#28238=CARTESIAN_POINT('',(-0.0134154,0.0373856238610512,0.0835291666666667));
#28239=CARTESIAN_POINT('',(-0.0153110694571917,0.0384800891324553,0.0836614583333334));
#28240=CARTESIAN_POINT('',(-0.0175,0.0384800891324554,0.08379375));
#28241=CARTESIAN_POINT('',(-0.0196889305428084,0.0384800891324553,0.0839260416666667));
#28242=CARTESIAN_POINT('',(-0.0215846,0.0373856238610512,0.0840583333333334));
#28243=CARTESIAN_POINT('',(-0.0234802694571917,0.036291158589647,0.084190625));
#28244=CARTESIAN_POINT('',(-0.0245747347285959,0.0343954891324554,0.0843229166666667));
#28245=CARTESIAN_POINT('',(-0.0256692000000001,0.0324998196752637,0.0844552083333334));
#28246=CARTESIAN_POINT('',(-0.0256692,0.0303108891324553,0.0845875));
#28247=CARTESIAN_POINT('',(-0.0256692000000001,0.028121958589647,0.0847197916666667));
#28248=CARTESIAN_POINT('',(-0.0245747347285959,0.0262262891324554,0.0848520833333334));
#28249=CARTESIAN_POINT('',(-0.0234802694571917,0.0243306196752637,0.0849843750000001));
#28250=CARTESIAN_POINT('',(-0.0215846,0.0232361544038595,0.0851166666666667));
#28251=CARTESIAN_POINT('',(-0.0196889305428084,0.0221416891324553,0.0852489583333334));
#28252=CARTESIAN_POINT('',(-0.0175,0.0221416891324554,0.08538125));
#28253=CARTESIAN_POINT('',(-0.0153110694571917,0.0221416891324553,0.0855135416666667));
#28254=CARTESIAN_POINT('',(-0.0134154,0.0232361544038595,0.0856458333333334));
#28255=CARTESIAN_POINT('',(-0.0115197305428084,0.0243306196752637,0.0857781250000001));
#28256=CARTESIAN_POINT('',(-0.0104252652714042,0.0262262891324554,0.0859104166666667));
#28257=CARTESIAN_POINT('',(-0.00933080000000005,0.028121958589647,0.0860427083333334));
#28258=CARTESIAN_POINT('',(-0.0093308,0.0303108891324553,0.086175));
#28259=CARTESIAN_POINT('',(-0.00933080000000005,0.0324998196752637,0.0863072916666667));
#28260=CARTESIAN_POINT('',(-0.0104252652714042,0.0343954891324554,0.0864395833333334));
#28261=CARTESIAN_POINT('',(-0.0115197305428084,0.036291158589647,0.086571875));
#28262=CARTESIAN_POINT('',(-0.0134154,0.0373856238610512,0.0867041666666667));
#28263=CARTESIAN_POINT('',(-0.0153110694571917,0.0384800891324553,0.0868364583333334));
#28264=CARTESIAN_POINT('',(-0.0175,0.0384800891324554,0.08696875));
#28265=CARTESIAN_POINT('',(-0.0196889305428084,0.0384800891324553,0.0871010416666667));
#28266=CARTESIAN_POINT('',(-0.0215846,0.0373856238610512,0.0872333333333334));
#28267=CARTESIAN_POINT('',(-0.0234802694571917,0.036291158589647,0.087365625));
#28268=CARTESIAN_POINT('',(-0.0245747347285959,0.0343954891324554,0.0874979166666667));
#28269=CARTESIAN_POINT('',(-0.0256692000000001,0.0324998196752637,0.0876302083333334));
#28270=CARTESIAN_POINT('',(-0.0256692,0.0303108891324553,0.0877625));
#28271=CARTESIAN_POINT('',(-0.0256692000000001,0.028121958589647,0.0878947916666667));
#28272=CARTESIAN_POINT('',(-0.0245747347285959,0.0262262891324554,0.0880270833333334));
#28273=CARTESIAN_POINT('',(-0.0234802694571917,0.0243306196752637,0.088159375));
#28274=CARTESIAN_POINT('',(-0.0215846,0.0232361544038595,0.0882916666666667));
#28275=CARTESIAN_POINT('',(-0.0196889305428084,0.0221416891324553,0.0884239583333334));
#28276=CARTESIAN_POINT('',(-0.0175,0.0221416891324554,0.08855625));
#28277=CARTESIAN_POINT('',(-0.0153110694571917,0.0221416891324553,0.0886885416666667));
#28278=CARTESIAN_POINT('',(-0.0134154,0.0232361544038595,0.0888208333333334));
#28279=CARTESIAN_POINT('',(-0.0115197305428084,0.0243306196752637,0.088953125));
#28280=CARTESIAN_POINT('',(-0.0104252652714042,0.0262262891324554,0.0890854166666667));
#28281=CARTESIAN_POINT('',(-0.00933080000000005,0.028121958589647,0.0892177083333334));
#28282=CARTESIAN_POINT('',(-0.0093308,0.0303108891324553,0.08935));
#28283=CARTESIAN_POINT('',(-0.00933080000000005,0.0324998196752637,0.0894822916666667));
#28284=CARTESIAN_POINT('',(-0.0104252652714042,0.0343954891324554,0.0896145833333333));
#28285=CARTESIAN_POINT('',(-0.0115197305428084,0.036291158589647,0.0897468750000001));
#28286=CARTESIAN_POINT('',(-0.0134154,0.0373856238610512,0.0898791666666667));
#28287=CARTESIAN_POINT('',(-0.0153110694571917,0.0384800891324553,0.0900114583333334));
#28288=CARTESIAN_POINT('',(-0.0175,0.0384800891324554,0.09014375));
#28289=CARTESIAN_POINT('',(-0.0196889305428084,0.0384800891324553,0.0902760416666667));
#28290=CARTESIAN_POINT('',(-0.0215846,0.0373856238610512,0.0904083333333334));
#28291=CARTESIAN_POINT('',(-0.0234802694571917,0.036291158589647,0.0905406250000001));
#28292=CARTESIAN_POINT('',(-0.0245747347285959,0.0343954891324554,0.0906729166666667));
#28293=CARTESIAN_POINT('',(-0.0256692000000001,0.0324998196752637,0.0908052083333334));
#28294=CARTESIAN_POINT('',(-0.0256692,0.0303108891324553,0.0909375));
#28295=CARTESIAN_POINT('',(-0.00933080000000004,0.0303108891324554,0.0827952040402267));
#28296=CARTESIAN_POINT('',(-0.00933080000000004,0.0324998196752636,0.0829274957068934));
#28297=CARTESIAN_POINT('',(-0.0104252652714042,0.0343954891324553,0.0830597873735601));
#28298=CARTESIAN_POINT('',(-0.0115197305428084,0.036291158589647,0.0831920790402268));
#28299=CARTESIAN_POINT('',(-0.0134154000000001,0.0373856238610512,0.0833243707068934));
#28300=CARTESIAN_POINT('',(-0.0153110694571917,0.0384800891324553,0.0834566623735601));
#28301=CARTESIAN_POINT('',(-0.0175000000000001,0.0384800891324554,0.0835889540402267));
#28302=CARTESIAN_POINT('',(-0.0196889305428084,0.0384800891324553,0.0837212457068933));
#28303=CARTESIAN_POINT('',(-0.0215846000000001,0.0373856238610512,0.0838535373735601));
#28304=CARTESIAN_POINT('',(-0.0234802694571917,0.036291158589647,0.0839858290402267));
#28305=CARTESIAN_POINT('',(-0.0245747347285959,0.0343954891324553,0.0841181207068934));
#28306=CARTESIAN_POINT('',(-0.0256692000000001,0.0324998196752636,0.08425041237356));
#28307=CARTESIAN_POINT('',(-0.0256692000000001,0.0303108891324554,0.0843827040402267));
#28308=CARTESIAN_POINT('',(-0.0256692000000001,0.028121958589647,0.0845149957068933));
#28309=CARTESIAN_POINT('',(-0.0245747347285959,0.0262262891324553,0.0846472873735601));
#28310=CARTESIAN_POINT('',(-0.0234802694571917,0.0243306196752637,0.0847795790402267));
#28311=CARTESIAN_POINT('',(-0.0215846000000001,0.0232361544038595,0.0849118707068934));
#28312=CARTESIAN_POINT('',(-0.0196889305428084,0.0221416891324553,0.08504416237356));
#28313=CARTESIAN_POINT('',(-0.0175000000000001,0.0221416891324553,0.0851764540402268));
#28314=CARTESIAN_POINT('',(-0.0153110694571917,0.0221416891324553,0.0853087457068933));
#28315=CARTESIAN_POINT('',(-0.0134154000000001,0.0232361544038595,0.0854410373735601));
#28316=CARTESIAN_POINT('',(-0.0115197305428084,0.0243306196752637,0.0855733290402267));
#28317=CARTESIAN_POINT('',(-0.0104252652714042,0.0262262891324553,0.0857056207068934));
#28318=CARTESIAN_POINT('',(-0.00933080000000003,0.028121958589647,0.08583791237356));
#28319=CARTESIAN_POINT('',(-0.00933080000000004,0.0303108891324554,0.0859702040402268));
#28320=CARTESIAN_POINT('',(-0.00933080000000004,0.0324998196752636,0.0861024957068934));
#28321=CARTESIAN_POINT('',(-0.0104252652714042,0.0343954891324553,0.0862347873735601));
#28322=CARTESIAN_POINT('',(-0.0115197305428084,0.036291158589647,0.0863670790402267));
#28323=CARTESIAN_POINT('',(-0.0134154000000001,0.0373856238610512,0.0864993707068934));
#28324=CARTESIAN_POINT('',(-0.0153110694571917,0.0384800891324553,0.08663166237356));
#28325=CARTESIAN_POINT('',(-0.0175000000000001,0.0384800891324554,0.0867639540402267));
#28326=CARTESIAN_POINT('',(-0.0196889305428084,0.0384800891324553,0.0868962457068933));
#28327=CARTESIAN_POINT('',(-0.0215846000000001,0.0373856238610512,0.08702853737356));
#28328=CARTESIAN_POINT('',(-0.0234802694571917,0.036291158589647,0.0871608290402267));
#28329=CARTESIAN_POINT('',(-0.0245747347285959,0.0343954891324553,0.0872931207068933));
#28330=CARTESIAN_POINT('',(-0.0256692000000001,0.0324998196752636,0.08742541237356));
#28331=CARTESIAN_POINT('',(-0.0256692000000001,0.0303108891324554,0.0875577040402268));
#28332=CARTESIAN_POINT('',(-0.0256692000000001,0.028121958589647,0.0876899957068934));
#28333=CARTESIAN_POINT('',(-0.0245747347285959,0.0262262891324553,0.08782228737356));
#28334=CARTESIAN_POINT('',(-0.0234802694571917,0.0243306196752637,0.0879545790402267));
#28335=CARTESIAN_POINT('',(-0.0215846000000001,0.0232361544038595,0.0880868707068934));
#28336=CARTESIAN_POINT('',(-0.0196889305428084,0.0221416891324553,0.08821916237356));
#28337=CARTESIAN_POINT('',(-0.0175000000000001,0.0221416891324553,0.0883514540402267));
#28338=CARTESIAN_POINT('',(-0.0153110694571917,0.0221416891324553,0.0884837457068934));
#28339=CARTESIAN_POINT('',(-0.0134154000000001,0.0232361544038595,0.08861603737356));
#28340=CARTESIAN_POINT('',(-0.0115197305428084,0.0243306196752637,0.0887483290402267));
#28341=CARTESIAN_POINT('',(-0.0104252652714042,0.0262262891324553,0.0888806207068934));
#28342=CARTESIAN_POINT('',(-0.00933080000000003,0.028121958589647,0.08901291237356));
#28343=CARTESIAN_POINT('',(-0.00933080000000004,0.0303108891324554,0.0891452040402267));
#28344=CARTESIAN_POINT('',(-0.00933080000000004,0.0324998196752636,0.0892774957068934));
#28345=CARTESIAN_POINT('',(-0.0104252652714042,0.0343954891324553,0.08940978737356));
#28346=CARTESIAN_POINT('',(-0.0115197305428084,0.036291158589647,0.0895420790402267));
#28347=CARTESIAN_POINT('',(-0.0134154000000001,0.0373856238610512,0.0896743707068934));
#28348=CARTESIAN_POINT('',(-0.0153110694571917,0.0384800891324553,0.0898066623735601));
#28349=CARTESIAN_POINT('',(-0.0175000000000001,0.0384800891324554,0.0899389540402267));
#28350=CARTESIAN_POINT('',(-0.0196889305428084,0.0384800891324553,0.0900712457068934));
#28351=CARTESIAN_POINT('',(-0.0215846000000001,0.0373856238610512,0.09020353737356));
#28352=CARTESIAN_POINT('',(-0.0234802694571917,0.036291158589647,0.0903358290402267));
#28353=CARTESIAN_POINT('',(-0.0245747347285959,0.0343954891324553,0.0904681207068934));
#28354=CARTESIAN_POINT('',(-0.0256692000000001,0.0324998196752636,0.0906004123735601));
#28355=CARTESIAN_POINT('',(-0.0256692000000001,0.0303108891324554,0.0907327040402267));
#28356=CARTESIAN_POINT('',(-0.00925242797917949,0.0303108891324554,0.0826059972446511));
#28357=CARTESIAN_POINT('',(-0.0092524279791795,0.0325208193949517,0.0827382889113178));
#28358=CARTESIAN_POINT('',(-0.0103573931104277,0.0344346751428656,0.0828705805779845));
#28359=CARTESIAN_POINT('',(-0.0114623582416759,0.0363485308907795,0.0830028722446511));
#28360=CARTESIAN_POINT('',(-0.0133762139895898,0.0374534960220277,0.0831351639113178));
#28361=CARTESIAN_POINT('',(-0.0152900697375036,0.0385584611532759,0.0832674555779845));
#28362=CARTESIAN_POINT('',(-0.0175000000000001,0.0385584611532759,0.0833997472446512));
#28363=CARTESIAN_POINT('',(-0.0197099302624964,0.0385584611532759,0.0835320389113178));
#28364=CARTESIAN_POINT('',(-0.0216237860104103,0.0374534960220277,0.0836643305779845));
#28365=CARTESIAN_POINT('',(-0.0235376417583242,0.0363485308907795,0.0837966222446511));
#28366=CARTESIAN_POINT('',(-0.0246426068895724,0.0344346751428656,0.0839289139113178));
#28367=CARTESIAN_POINT('',(-0.0257475720208206,0.0325208193949517,0.0840612055779845));
#28368=CARTESIAN_POINT('',(-0.0257475720208206,0.0303108891324554,0.0841934972446512));
#28369=CARTESIAN_POINT('',(-0.0257475720208206,0.0281009588699589,0.0843257889113178));
#28370=CARTESIAN_POINT('',(-0.0246426068895724,0.026187103122045,0.0844580805779845));
#28371=CARTESIAN_POINT('',(-0.0235376417583242,0.0242732473741312,0.0845903722446511));
#28372=CARTESIAN_POINT('',(-0.0216237860104103,0.023168282242883,0.0847226639113178));
#28373=CARTESIAN_POINT('',(-0.0197099302624964,0.0220633171116348,0.0848549555779845));
#28374=CARTESIAN_POINT('',(-0.0175000000000001,0.0220633171116348,0.0849872472446512));
#28375=CARTESIAN_POINT('',(-0.0152900697375036,0.0220633171116348,0.0851195389113178));
#28376=CARTESIAN_POINT('',(-0.0133762139895898,0.023168282242883,0.0852518305779845));
#28377=CARTESIAN_POINT('',(-0.0114623582416759,0.0242732473741312,0.0853841222446512));
#28378=CARTESIAN_POINT('',(-0.0103573931104277,0.026187103122045,0.0855164139113179));
#28379=CARTESIAN_POINT('',(-0.0092524279791795,0.0281009588699589,0.0856487055779845));
#28380=CARTESIAN_POINT('',(-0.00925242797917949,0.0303108891324554,0.0857809972446512));
#28381=CARTESIAN_POINT('',(-0.0092524279791795,0.0325208193949517,0.0859132889113178));
#28382=CARTESIAN_POINT('',(-0.0103573931104277,0.0344346751428656,0.0860455805779845));
#28383=CARTESIAN_POINT('',(-0.0114623582416759,0.0363485308907795,0.0861778722446511));
#28384=CARTESIAN_POINT('',(-0.0133762139895898,0.0374534960220277,0.0863101639113179));
#28385=CARTESIAN_POINT('',(-0.0152900697375036,0.0385584611532759,0.0864424555779845));
#28386=CARTESIAN_POINT('',(-0.0175000000000001,0.0385584611532759,0.0865747472446512));
#28387=CARTESIAN_POINT('',(-0.0197099302624964,0.0385584611532759,0.0867070389113178));
#28388=CARTESIAN_POINT('',(-0.0216237860104103,0.0374534960220277,0.0868393305779845));
#28389=CARTESIAN_POINT('',(-0.0235376417583242,0.0363485308907795,0.0869716222446512));
#28390=CARTESIAN_POINT('',(-0.0246426068895724,0.0344346751428656,0.0871039139113179));
#28391=CARTESIAN_POINT('',(-0.0257475720208206,0.0325208193949517,0.0872362055779845));
#28392=CARTESIAN_POINT('',(-0.0257475720208206,0.0303108891324554,0.0873684972446512));
#28393=CARTESIAN_POINT('',(-0.0257475720208206,0.0281009588699589,0.0875007889113178));
#28394=CARTESIAN_POINT('',(-0.0246426068895724,0.026187103122045,0.0876330805779846));
#28395=CARTESIAN_POINT('',(-0.0235376417583242,0.0242732473741312,0.0877653722446512));
#28396=CARTESIAN_POINT('',(-0.0216237860104103,0.023168282242883,0.0878976639113178));
#28397=CARTESIAN_POINT('',(-0.0197099302624964,0.0220633171116348,0.0880299555779845));
#28398=CARTESIAN_POINT('',(-0.0175000000000001,0.0220633171116348,0.0881622472446511));
#28399=CARTESIAN_POINT('',(-0.0152900697375036,0.0220633171116348,0.0882945389113178));
#28400=CARTESIAN_POINT('',(-0.0133762139895898,0.023168282242883,0.0884268305779846));
#28401=CARTESIAN_POINT('',(-0.0114623582416759,0.0242732473741312,0.0885591222446512));
#28402=CARTESIAN_POINT('',(-0.0103573931104277,0.026187103122045,0.0886914139113178));
#28403=CARTESIAN_POINT('',(-0.0092524279791795,0.0281009588699589,0.0888237055779845));
#28404=CARTESIAN_POINT('',(-0.00925242797917949,0.0303108891324554,0.0889559972446511));
#28405=CARTESIAN_POINT('',(-0.0092524279791795,0.0325208193949517,0.0890882889113179));
#28406=CARTESIAN_POINT('',(-0.0103573931104277,0.0344346751428656,0.0892205805779845));
#28407=CARTESIAN_POINT('',(-0.0114623582416759,0.0363485308907795,0.0893528722446512));
#28408=CARTESIAN_POINT('',(-0.0133762139895898,0.0374534960220277,0.0894851639113178));
#28409=CARTESIAN_POINT('',(-0.0152900697375036,0.0385584611532759,0.0896174555779845));
#28410=CARTESIAN_POINT('',(-0.0175000000000001,0.0385584611532759,0.0897497472446512));
#28411=CARTESIAN_POINT('',(-0.0197099302624964,0.0385584611532759,0.0898820389113179));
#28412=CARTESIAN_POINT('',(-0.0216237860104103,0.0374534960220277,0.0900143305779845));
#28413=CARTESIAN_POINT('',(-0.0235376417583242,0.0363485308907795,0.0901466222446512));
#28414=CARTESIAN_POINT('',(-0.0246426068895724,0.0344346751428656,0.0902789139113178));
#28415=CARTESIAN_POINT('',(-0.0257475720208206,0.0325208193949517,0.0904112055779845));
#28416=CARTESIAN_POINT('',(-0.0257475720208206,0.0303108891324554,0.0905434972446512));
#28417=CARTESIAN_POINT('',(-0.00910761536726419,0.0303108891324553,0.0824611846327359));
#28418=CARTESIAN_POINT('',(-0.00910761536726419,0.0325596218173683,0.0825934762994026));
#28419=CARTESIAN_POINT('',(-0.0102319817097207,0.0345070814488233,0.0827257679660692));
#28420=CARTESIAN_POINT('',(-0.0113563480521771,0.0364545410802783,0.0828580596327359));
#28421=CARTESIAN_POINT('',(-0.0133038076836321,0.0375789074227348,0.0829903512994025));
#28422=CARTESIAN_POINT('',(-0.0152512673150871,0.0387032737651912,0.0831226429660692));
#28423=CARTESIAN_POINT('',(-0.0175,0.0387032737651912,0.0832549346327359));
#28424=CARTESIAN_POINT('',(-0.019748732684913,0.0387032737651912,0.0833872262994025));
#28425=CARTESIAN_POINT('',(-0.021696192316368,0.0375789074227348,0.0835195179660692));
#28426=CARTESIAN_POINT('',(-0.023643651947823,0.0364545410802783,0.083651809632736));
#28427=CARTESIAN_POINT('',(-0.0247680182902794,0.0345070814488233,0.0837841012994025));
#28428=CARTESIAN_POINT('',(-0.0258923846327359,0.0325596218173683,0.0839163929660693));
#28429=CARTESIAN_POINT('',(-0.0258923846327359,0.0303108891324553,0.0840486846327359));
#28430=CARTESIAN_POINT('',(-0.0258923846327359,0.0280621564475424,0.0841809762994026));
#28431=CARTESIAN_POINT('',(-0.0247680182902794,0.0261146968160874,0.0843132679660692));
#28432=CARTESIAN_POINT('',(-0.023643651947823,0.0241672371846324,0.0844455596327359));
#28433=CARTESIAN_POINT('',(-0.021696192316368,0.023042870842176,0.0845778512994025));
#28434=CARTESIAN_POINT('',(-0.019748732684913,0.0219185044997195,0.0847101429660692));
#28435=CARTESIAN_POINT('',(-0.0175,0.0219185044997195,0.0848424346327359));
#28436=CARTESIAN_POINT('',(-0.0152512673150871,0.0219185044997195,0.0849747262994025));
#28437=CARTESIAN_POINT('',(-0.0133038076836321,0.023042870842176,0.0851070179660692));
#28438=CARTESIAN_POINT('',(-0.0113563480521771,0.0241672371846324,0.0852393096327359));
#28439=CARTESIAN_POINT('',(-0.0102319817097207,0.0261146968160874,0.0853716012994025));
#28440=CARTESIAN_POINT('',(-0.00910761536726419,0.0280621564475424,0.0855038929660693));
#28441=CARTESIAN_POINT('',(-0.00910761536726419,0.0303108891324553,0.0856361846327359));
#28442=CARTESIAN_POINT('',(-0.00910761536726419,0.0325596218173683,0.0857684762994026));
#28443=CARTESIAN_POINT('',(-0.0102319817097207,0.0345070814488233,0.0859007679660692));
#28444=CARTESIAN_POINT('',(-0.0113563480521771,0.0364545410802783,0.0860330596327359));
#28445=CARTESIAN_POINT('',(-0.0133038076836321,0.0375789074227348,0.0861653512994025));
#28446=CARTESIAN_POINT('',(-0.0152512673150871,0.0387032737651912,0.0862976429660692));
#28447=CARTESIAN_POINT('',(-0.0175,0.0387032737651912,0.0864299346327359));
#28448=CARTESIAN_POINT('',(-0.019748732684913,0.0387032737651912,0.0865622262994026));
#28449=CARTESIAN_POINT('',(-0.021696192316368,0.0375789074227348,0.0866945179660692));
#28450=CARTESIAN_POINT('',(-0.023643651947823,0.0364545410802783,0.0868268096327359));
#28451=CARTESIAN_POINT('',(-0.0247680182902794,0.0345070814488233,0.0869591012994025));
#28452=CARTESIAN_POINT('',(-0.0258923846327359,0.0325596218173683,0.0870913929660692));
#28453=CARTESIAN_POINT('',(-0.0258923846327359,0.0303108891324553,0.0872236846327359));
#28454=CARTESIAN_POINT('',(-0.0258923846327359,0.0280621564475424,0.0873559762994026));
#28455=CARTESIAN_POINT('',(-0.0247680182902794,0.0261146968160874,0.0874882679660692));
#28456=CARTESIAN_POINT('',(-0.023643651947823,0.0241672371846324,0.0876205596327359));
#28457=CARTESIAN_POINT('',(-0.021696192316368,0.023042870842176,0.0877528512994025));
#28458=CARTESIAN_POINT('',(-0.019748732684913,0.0219185044997195,0.0878851429660692));
#28459=CARTESIAN_POINT('',(-0.0175,0.0219185044997195,0.0880174346327359));
#28460=CARTESIAN_POINT('',(-0.0152512673150871,0.0219185044997195,0.0881497262994026));
#28461=CARTESIAN_POINT('',(-0.0133038076836321,0.023042870842176,0.0882820179660692));
#28462=CARTESIAN_POINT('',(-0.0113563480521771,0.0241672371846324,0.0884143096327359));
#28463=CARTESIAN_POINT('',(-0.0102319817097207,0.0261146968160874,0.0885466012994025));
#28464=CARTESIAN_POINT('',(-0.00910761536726419,0.0280621564475424,0.0886788929660693));
#28465=CARTESIAN_POINT('',(-0.00910761536726419,0.0303108891324553,0.0888111846327359));
#28466=CARTESIAN_POINT('',(-0.00910761536726419,0.0325596218173683,0.0889434762994026));
#28467=CARTESIAN_POINT('',(-0.0102319817097207,0.0345070814488233,0.0890757679660692));
#28468=CARTESIAN_POINT('',(-0.0113563480521771,0.0364545410802783,0.0892080596327359));
#28469=CARTESIAN_POINT('',(-0.0133038076836321,0.0375789074227348,0.0893403512994025));
#28470=CARTESIAN_POINT('',(-0.0152512673150871,0.0387032737651912,0.0894726429660692));
#28471=CARTESIAN_POINT('',(-0.0175,0.0387032737651912,0.0896049346327359));
#28472=CARTESIAN_POINT('',(-0.019748732684913,0.0387032737651912,0.0897372262994026));
#28473=CARTESIAN_POINT('',(-0.021696192316368,0.0375789074227348,0.0898695179660692));
#28474=CARTESIAN_POINT('',(-0.023643651947823,0.0364545410802783,0.0900018096327359));
#28475=CARTESIAN_POINT('',(-0.0247680182902794,0.0345070814488233,0.0901341012994025));
#28476=CARTESIAN_POINT('',(-0.0258923846327359,0.0325596218173683,0.0902663929660692));
#28477=CARTESIAN_POINT('',(-0.0258923846327359,0.0303108891324553,0.0903986846327359));
#28478=CARTESIAN_POINT('',(-0.0093308,0.0303108891324553,0.083));
#28479=CARTESIAN_POINT('',(-0.00933080000000005,0.0324998196752637,0.0831322916666668));
#28480=CARTESIAN_POINT('',(-0.0104252652714042,0.0343954891324554,0.0832645833333334));
#28481=CARTESIAN_POINT('',(-0.0115197305428084,0.036291158589647,0.0833968750000001));
#28482=CARTESIAN_POINT('',(-0.0134154,0.0373856238610512,0.0835291666666667));
#28483=CARTESIAN_POINT('',(-0.0153110694571917,0.0384800891324553,0.0836614583333334));
#28484=CARTESIAN_POINT('',(-0.0175,0.0384800891324554,0.08379375));
#28485=CARTESIAN_POINT('',(-0.0196889305428084,0.0384800891324553,0.0839260416666667));
#28486=CARTESIAN_POINT('',(-0.0215846,0.0373856238610512,0.0840583333333334));
#28487=CARTESIAN_POINT('',(-0.0234802694571917,0.036291158589647,0.084190625));
#28488=CARTESIAN_POINT('',(-0.0245747347285959,0.0343954891324554,0.0843229166666667));
#28489=CARTESIAN_POINT('',(-0.0256692000000001,0.0324998196752636,0.0844552083333334));
#28490=CARTESIAN_POINT('',(-0.0256692,0.0303108891324553,0.0845875));
#28491=CARTESIAN_POINT('',(-0.0093308,0.0303108891324553,0.083));
#28492=CARTESIAN_POINT('',(-0.0256692,0.0303108891324553,0.0845875));
#28493=CARTESIAN_POINT('',(-0.0093308,0.0303108891324553,0.083));
#28494=CARTESIAN_POINT('',(-0.00933080000000005,0.0317860674431147,0.083));
#28495=CARTESIAN_POINT('',(-0.0101154411361515,0.0347108515037046,0.0830000000000001));
#28496=CARTESIAN_POINT('',(-0.012199646341259,0.0368722439921494,0.083));
#28497=CARTESIAN_POINT('',(-0.0134462729974218,0.0376593187070208,0.083));
#28498=CARTESIAN_POINT('',(-0.0264312,0.0303108891324553,0.0909375));
#28499=CARTESIAN_POINT('',(-0.0256692,0.0303108891324553,0.0909375));
#28500=CARTESIAN_POINT('',(-0.0093308,0.0303108891324553,0.08935));
#28501=CARTESIAN_POINT('',(-0.00933080000000003,0.0324998196752637,0.0894822916666667));
#28502=CARTESIAN_POINT('',(-0.0104252652714042,0.0343954891324554,0.0896145833333333));
#28503=CARTESIAN_POINT('',(-0.0115197305428084,0.036291158589647,0.0897468750000001));
#28504=CARTESIAN_POINT('',(-0.0134154,0.0373856238610512,0.0898791666666667));
#28505=CARTESIAN_POINT('',(-0.0153110694571917,0.0384800891324553,0.0900114583333334));
#28506=CARTESIAN_POINT('',(-0.0175,0.0384800891324554,0.09014375));
#28507=CARTESIAN_POINT('',(-0.0196889305428084,0.0384800891324553,0.0902760416666667));
#28508=CARTESIAN_POINT('',(-0.0215846,0.0373856238610512,0.0904083333333334));
#28509=CARTESIAN_POINT('',(-0.0234802694571917,0.036291158589647,0.0905406250000001));
#28510=CARTESIAN_POINT('',(-0.0245747347285959,0.0343954891324554,0.0906729166666667));
#28511=CARTESIAN_POINT('',(-0.0256692000000001,0.0324998196752637,0.0908052083333334));
#28512=CARTESIAN_POINT('',(-0.0256692,0.0303108891324553,0.0909375));
#28513=CARTESIAN_POINT('',(-0.0093308,0.0303108891324553,0.08935));
#28514=CARTESIAN_POINT('',(-0.0256692,0.0303108891324553,0.0877625));
#28515=CARTESIAN_POINT('',(-0.0256692,0.028121958589647,0.0878947916666667));
#28516=CARTESIAN_POINT('',(-0.0245747347285959,0.0262262891324554,0.0880270833333334));
#28517=CARTESIAN_POINT('',(-0.0234802694571917,0.0243306196752637,0.088159375));
#28518=CARTESIAN_POINT('',(-0.0215846,0.0232361544038595,0.0882916666666667));
#28519=CARTESIAN_POINT('',(-0.0196889305428084,0.0221416891324553,0.0884239583333334));
#28520=CARTESIAN_POINT('',(-0.0175,0.0221416891324554,0.08855625));
#28521=CARTESIAN_POINT('',(-0.0153110694571917,0.0221416891324553,0.0886885416666667));
#28522=CARTESIAN_POINT('',(-0.0134154,0.0232361544038595,0.0888208333333334));
#28523=CARTESIAN_POINT('',(-0.0115197305428084,0.0243306196752637,0.088953125));
#28524=CARTESIAN_POINT('',(-0.0104252652714042,0.0262262891324554,0.0890854166666667));
#28525=CARTESIAN_POINT('',(-0.00933080000000006,0.028121958589647,0.0892177083333334));
#28526=CARTESIAN_POINT('',(-0.0093308,0.0303108891324553,0.08935));
#28527=CARTESIAN_POINT('',(-0.0256692,0.0303108891324553,0.0877625));
#28528=CARTESIAN_POINT('',(-0.0093308,0.0303108891324553,0.086175));
#28529=CARTESIAN_POINT('',(-0.00933080000000004,0.0324998196752637,0.0863072916666667));
#28530=CARTESIAN_POINT('',(-0.0104252652714042,0.0343954891324554,0.0864395833333334));
#28531=CARTESIAN_POINT('',(-0.0115197305428084,0.036291158589647,0.086571875));
#28532=CARTESIAN_POINT('',(-0.0134154,0.0373856238610512,0.0867041666666667));
#28533=CARTESIAN_POINT('',(-0.0153110694571917,0.0384800891324553,0.0868364583333334));
#28534=CARTESIAN_POINT('',(-0.0175,0.0384800891324554,0.08696875));
#28535=CARTESIAN_POINT('',(-0.0196889305428084,0.0384800891324553,0.0871010416666667));
#28536=CARTESIAN_POINT('',(-0.0215846,0.0373856238610512,0.0872333333333334));
#28537=CARTESIAN_POINT('',(-0.0234802694571917,0.036291158589647,0.087365625));
#28538=CARTESIAN_POINT('',(-0.0245747347285959,0.0343954891324554,0.0874979166666667));
#28539=CARTESIAN_POINT('',(-0.0256692000000001,0.0324998196752637,0.0876302083333333));
#28540=CARTESIAN_POINT('',(-0.0256692,0.0303108891324553,0.0877625));
#28541=CARTESIAN_POINT('',(-0.0093308,0.0303108891324553,0.086175));
#28542=CARTESIAN_POINT('',(-0.0256692,0.0303108891324553,0.0845875));
#28543=CARTESIAN_POINT('',(-0.0256692,0.028121958589647,0.0847197916666667));
#28544=CARTESIAN_POINT('',(-0.0245747347285959,0.0262262891324554,0.0848520833333334));
#28545=CARTESIAN_POINT('',(-0.0234802694571917,0.0243306196752637,0.0849843750000001));
#28546=CARTESIAN_POINT('',(-0.0215846,0.0232361544038595,0.0851166666666667));
#28547=CARTESIAN_POINT('',(-0.0196889305428084,0.0221416891324553,0.0852489583333334));
#28548=CARTESIAN_POINT('',(-0.0175,0.0221416891324554,0.08538125));
#28549=CARTESIAN_POINT('',(-0.0153110694571917,0.0221416891324553,0.0855135416666667));
#28550=CARTESIAN_POINT('',(-0.0134154,0.0232361544038595,0.0856458333333334));
#28551=CARTESIAN_POINT('',(-0.0115197305428084,0.0243306196752637,0.0857781250000001));
#28552=CARTESIAN_POINT('',(-0.0104252652714042,0.0262262891324554,0.0859104166666667));
#28553=CARTESIAN_POINT('',(-0.00933080000000005,0.028121958589647,0.0860427083333333));
#28554=CARTESIAN_POINT('',(-0.0093308,0.0303108891324553,0.086175));
#28555=CARTESIAN_POINT('',(-0.0256835799347999,0.0303108891324553,0.0883593889197018));
#28556=CARTESIAN_POINT('',(-0.0256692,0.0303108891324553,0.093));
#28557=CARTESIAN_POINT('',(-0.0175,0.0303108891324553,0.083));
#28558=CARTESIAN_POINT('',(-0.0175,0.0303108891324553,0.083));
#28559=CARTESIAN_POINT('',(-0.0175,0.0303108891324553,0.093));
#28560=CARTESIAN_POINT('',(-0.0175,0.0303108891324553,0.093));
#28561=CARTESIAN_POINT('',(-0.0256692,0.0303108891324553,0.093));
#28562=CARTESIAN_POINT('',(-0.0175,0.0303108891324553,0.093));
#45463=MECHANICAL_DESIGN_GEOMETRIC_PRESENTATION_REPRESENTATION('',(#13532),#45464);
#45464=(
GEOMETRIC_REPRESENTATION_CONTEXT(3)
GLOBAL_UNCERTAINTY_ASSIGNED_CONTEXT((#45492))
GLOBAL_UNIT_ASSIGNED_CONTEXT((#45522,#45521,#45520))
REPRESENTATION_CONTEXT('MAS-690','TOP_LEVEL_ASSEMBLY_PART')
);
#45468=(
GEOMETRIC_REPRESENTATION_CONTEXT(3)
GLOBAL_UNCERTAINTY_ASSIGNED_CONTEXT((#45496))
GLOBAL_UNIT_ASSIGNED_CONTEXT((#45522,#45521,#45520))
REPRESENTATION_CONTEXT('refill_cap','COMPONENT_PART')
);
#45492=UNCERTAINTY_MEASURE_WITH_UNIT(LENGTH_MEASURE(1.E-8),#45522,
'DISTANCE_ACCURACY_VALUE','Maximum Tolerance applied to model');
#45496=UNCERTAINTY_MEASURE_WITH_UNIT(LENGTH_MEASURE(2.E-5),#45522,
'DISTANCE_ACCURACY_VALUE','Maximum Tolerance applied to model');
#45520=(
NAMED_UNIT(*)
SI_UNIT($,.STERADIAN.)
SOLID_ANGLE_UNIT()
);
#45521=(
NAMED_UNIT(*)
PLANE_ANGLE_UNIT()
SI_UNIT($,.RADIAN.)
);
#45522=(
LENGTH_UNIT()
NAMED_UNIT(*)
SI_UNIT($,.METRE.)
);
#45530=PRODUCT_DEFINITION_SHAPE('','',#45589);
#45589=PRODUCT_DEFINITION('','',#45645,#45617);
#45617=PRODUCT_DEFINITION_CONTEXT('',#45782,'design');
#45645=PRODUCT_DEFINITION_FORMATION_WITH_SPECIFIED_SOURCE('','',#45701,
 .NOT_KNOWN.);
#45701=PRODUCT('refill_cap','refill_cap','refill_cap',(#45757));
#45757=PRODUCT_CONTEXT('',#45782,'mechanical');
#45782=APPLICATION_CONTEXT('managed model based 3d engineering');
ENDSEC;
END-ISO-10303-21;
